ISO-10303-21;
HEADER;
FILE_DESCRIPTION (('STEP AP214'),
    '1' );
FILE_NAME ('hex flange nut gradea_iso_ISO - 4161 - M5 - N.step',
    '2026-10-25T17:17:34',
    ( '' ),
    ( '' ),
    'SwSTEP 2.0',
    'SolidWorks 2026',
    '' );
FILE_SCHEMA (( 'AUTOMOTIVE_DESIGN' ));
ENDSEC;

DATA;
#7=( BOUNDED_SURFACE ( )  B_SPLINE_SURFACE ( 3, 2, ( 
 ( #3858, #16070, #12849 ),
 ( #17539, #18820, #1124 ),
 ( #12942, #8258, #11381 ),
 ( #11576, #9821, #15783 ),
 ( #19010, #5241, #9923 ),
 ( #17252, #845, #14308 ) ),
 .UNSPECIFIED., .F., .F., .F. ) 
 B_SPLINE_SURFACE_WITH_KNOTS ( ( 4, 2, 4 ),
 ( 3, 3 ),
 ( 0.02032853247518126918, 0.02278863295364821906, 0.02524873343211517240 ),
 ( 0.000000000000000000, 1.000000000000000000 ),
 .UNSPECIFIED. ) 
 GEOMETRIC_REPRESENTATION_ITEM ( )  RATIONAL_B_SPLINE_SURFACE ( (
 ( 1.000000000000000000, 0.8047781615896837382, 1.000000000000000000),
 ( 1.000000000000000000, 0.8123767586289252218, 1.000000000000000000),
 ( 1.000000000000000000, 0.8190662415564388121, 1.000000000000000000),
 ( 1.000000000000000000, 0.8192361015669026303, 1.000000000000000000),
 ( 1.000000000000000000, 0.8126135807103900266, 1.000000000000000000),
 ( 1.000000000000000000, 0.8047712338318593339, 1.000000000000000000) ) ) 
 REPRESENTATION_ITEM ( '' )  SURFACE ( )  );
#15=CARTESIAN_POINT ( 'NONE',  ( -4.204015924366189871, 1.626724848190922446, -3.610627190413390419 ) ) ;
#26=CARTESIAN_POINT ( 'NONE',  ( 0.000000000000000000, 0.000000000000000000, -0.2800830152838844622 ) ) ;
#31=CARTESIAN_POINT ( 'NONE',  ( 1.287237434362044075, 3.875615274277557809, -3.430618716626812059 ) ) ;
#35=CARTESIAN_POINT ( 'NONE',  ( 0.000000000000000000, 0.000000000000000000, -25.03750572909317285 ) ) ;
#86=ORIENTED_EDGE ( 'NONE', *, *, #4961, .F. ) ;
#94=APPLICATION_CONTEXT ( 'automotive_design' ) ;
#161=EDGE_CURVE ( 'NONE', #11737, #9031, #8962, .T. ) ;
#167=DIRECTION ( 'NONE',  ( 0.000000000000000000, 0.000000000000000000, 1.000000000000000000 ) ) ;
#178=EDGE_CURVE ( 'NONE', #2762, #9031, #12708, .T. ) ;
#183=CARTESIAN_POINT ( 'NONE',  ( 4.000000000000000000, 2.512223110932545023, -3.469391141908803711 ) ) ;
#187=EDGE_CURVE ( 'NONE', #10576, #17634, #10361, .T. ) ;
#193=CARTESIAN_POINT ( 'NONE',  ( -5.384454397937118664, 6.702023979852544604E-16, -5.000000000000000000 ) ) ;
#225=CARTESIAN_POINT ( 'NONE',  ( 3.453038570460273071, 2.625189405340834448, -3.535263753543585352 ) ) ;
#230=ORIENTED_EDGE ( 'NONE', *, *, #9491, .F. ) ;
#261=CARTESIAN_POINT ( 'NONE',  ( -1.999999999999999556, 3.464101615137754830, -3.142992957459232795 ) ) ;
#265=CARTESIAN_POINT ( 'NONE',  ( -2.100000000000000089, 2.571758278209441957E-16, -5.000000000000000000 ) ) ;
#266=AXIS2_PLACEMENT_3D ( 'NONE', #8263, #12758, #18727 ) ;
#284=CARTESIAN_POINT ( 'NONE',  ( -0.5449313310646672903, -4.304185902836978883, -3.316620875263469159 ) ) ;
#289=CONICAL_SURFACE ( 'NONE', #10266, 4.000000000000000000, 0.8911886515913786111 ) ;
#308=CARTESIAN_POINT ( 'NONE',  ( -4.000000000000000000, 2.511478553582031203, -3.469254451724764543 ) ) ;
#335=ORIENTED_EDGE ( 'NONE', *, *, #6417, .T. ) ;
#368=ORIENTED_EDGE ( 'NONE', *, *, #16035, .T. ) ;
#378=FACE_OUTER_BOUND ( 'NONE', #12586, .T. ) ;
#386=FACE_OUTER_BOUND ( 'NONE', #3807, .T. ) ;
#398=CARTESIAN_POINT ( 'NONE',  ( 4.211140560182196957, 2.431303136016536470, -3.745885042887433514 ) ) ;
#425=CARTESIAN_POINT ( 'NONE',  ( 2.000000000000005329, -3.464101615137751722, 0.000000000000000000 ) ) ;
#499=CARTESIAN_POINT ( 'NONE',  ( -4.000000000000000000, -2.309401076758515803, -0.4999999999999995559 ) ) ;
#510=AXIS2_PLACEMENT_3D ( 'NONE', #5921, #13234, #11867 ) ;
#511=CARTESIAN_POINT ( 'NONE',  ( 4.197393957002303999, 7.772902908466098641E-14, -3.503767560748929810 ) ) ;
#556=ORIENTED_EDGE ( 'NONE', *, *, #12119, .F. ) ;
#566=CARTESIAN_POINT ( 'NONE',  ( 2.805705207896068476, -3.226868319750173075, -3.503898532754370354 ) ) ;
#573=ORIENTED_EDGE ( 'NONE', *, *, #9703, .F. ) ;
#575=CARTESIAN_POINT ( 'NONE',  ( -6.259644161404860030E-16, -4.618802153517027165, -5.000000000000000000 ) ) ;
#582=VECTOR ( 'NONE', #10959, 1000.000000000000227 ) ;
#598=CARTESIAN_POINT ( 'NONE',  ( -4.000000000000000000, 0.1981133338132459731, 2.096406544454392723E-17 ) ) ;
#614=FACE_OUTER_BOUND ( 'NONE', #13488, .T. ) ;
#663=ADVANCED_FACE ( 'NONE', ( #13403 ), #5985, .F. ) ;
#664=CARTESIAN_POINT ( 'NONE',  ( 0.000000000000000000, 0.000000000000000000, -5.000000000000000000 ) ) ;
#665=CARTESIAN_POINT ( 'NONE',  ( -2.100000000000000089, 2.571758278209441957E-16, -4.694516984716113228 ) ) ;
#672=DIRECTION ( 'NONE',  ( 0.8660254037844379305, 0.5000000000000013323, 0.000000000000000000 ) ) ;
#685=EDGE_LOOP ( 'NONE', ( #18840, #966, #7472, #17589 ) ) ;
#709=CARTESIAN_POINT ( 'NONE',  ( 0.3208286057739604957, -4.433571671609698228, -0.3503314178412692548 ) ) ;
#722=CARTESIAN_POINT ( 'NONE',  ( -3.680118525130244400, 2.494084732383327285, -0.3507732604232449702 ) ) ;
#758=CARTESIAN_POINT ( 'NONE',  ( 4.211140560182196957, -2.431303136016555122, -3.745885042887436622 ) ) ;
#770=EDGE_CURVE ( 'NONE', #14464, #4492, #1482, .T. ) ;
#771=EDGE_LOOP ( 'NONE', ( #14055, #7466, #18393 ) ) ;
#782=EDGE_CURVE ( 'NONE', #14464, #6163, #17546, .T. ) ;
#803=CARTESIAN_POINT ( 'NONE',  ( -4.211140560182196957, 2.431303136016537803, -3.745885042887433514 ) ) ;
#808=ORIENTED_EDGE ( 'NONE', *, *, #18816, .F. ) ;
#822=ORIENTED_EDGE ( 'NONE', *, *, #3264, .T. ) ;
#845=CARTESIAN_POINT ( 'NONE',  ( 4.141042297810615835, -2.227970268150433863, -3.687027686973623819 ) ) ;
#852=DIRECTION ( 'NONE',  ( 0.000000000000000000, 0.000000000000000000, 1.000000000000000000 ) ) ;
#871=VECTOR ( 'NONE', #3828, 1000.000000000000000 ) ;
#874=FACE_OUTER_BOUND ( 'NONE', #685, .T. ) ;
#900=CARTESIAN_POINT ( 'NONE',  ( -0.3461262719736137305, 4.658553426539289610, -3.671615880910373608 ) ) ;
#907=DIRECTION ( 'NONE',  ( -0.000000000000000000, -0.000000000000000000, 1.000000000000000000 ) ) ;
#908=EDGE_CURVE ( 'NONE', #13473, #10972, #10673, .T. ) ;
#911=CARTESIAN_POINT ( 'NONE',  ( 4.203833317240879275, 1.627343821129582979, -3.597273115243889929 ) ) ;
#925=EDGE_CURVE ( 'NONE', #14097, #6590, #7774, .T. ) ;
#947=UNCERTAINTY_MEASURE_WITH_UNIT (LENGTH_MEASURE( 1.000000000000000082E-05 ), #8507, 'distance_accuracy_value', 'NONE');
#958=CARTESIAN_POINT ( 'NONE',  ( 1.567478505476134803E-15, 4.618802153517012954, -3.504269196027872457 ) ) ;
#965=CARTESIAN_POINT ( 'NONE',  ( 5.384454397937118664, 0.000000000000000000, -4.484454397937119197 ) ) ;
#966=ORIENTED_EDGE ( 'NONE', *, *, #1251, .T. ) ;
#1008=CARTESIAN_POINT ( 'NONE',  ( 0.000000000000000000, 0.000000000000000000, -4.974599999999998801 ) ) ;
#1047=CARTESIAN_POINT ( 'NONE',  ( 0.6920835326022565237, 4.454600218803884459, -3.597382984111579862 ) ) ;
#1048=EDGE_CURVE ( 'NONE', #18266, #6163, #11022, .T. ) ;
#1060=CARTESIAN_POINT ( 'NONE',  ( 0.000000000000000000, 0.000000000000000000, 0.000000000000000000 ) ) ;
#1100=CARTESIAN_POINT ( 'NONE',  ( -3.455068668934486276, 2.624017327439035707, -3.316620875263955437 ) ) ;
#1111=AXIS2_PLACEMENT_3D ( 'NONE', #1706, #12161, #6016 ) ;
#1124=CARTESIAN_POINT ( 'NONE',  ( 0.6640947660595348800, -4.471078309994175548, -3.602146406945708090 ) ) ;
#1127=AXIS2_PLACEMENT_3D ( 'NONE', #14079, #907, #2259 ) ;
#1133=CARTESIAN_POINT ( 'NONE',  ( 0.000000000000000000, 0.000000000000000000, -25.03750572909317285 ) ) ;
#1134=CARTESIAN_POINT ( 'NONE',  ( -4.000000000000000000, -2.309401076758515803, -0.4999999999999995559 ) ) ;
#1136=EDGE_CURVE ( 'NONE', #1970, #5897, #16626, .T. ) ;
#1139=DIRECTION ( 'NONE',  ( -0.5000000000000019984, -0.8660254037844375974, 0.000000000000000000 ) ) ;
#1147=DIRECTION ( 'NONE',  ( 0.000000000000000000, 0.000000000000000000, -1.000000000000000000 ) ) ;
#1160=DIRECTION ( 'NONE',  ( -0.000000000000000000, -0.000000000000000000, 1.000000000000000000 ) ) ;
#1183=CARTESIAN_POINT ( 'NONE',  ( -4.197393957002303999, 0.4069871074557429025, -3.503767560748926257 ) ) ;
#1189=CARTESIAN_POINT ( 'NONE',  ( -3.999999999999999112, 1.539600717838996324, -3.300726591567078039 ) ) ;
#1239=CARTESIAN_POINT ( 'NONE',  ( 4.000000000000000000, -2.309401076758514915, -3.433295621305383349 ) ) ;
#1251=EDGE_CURVE ( 'NONE', #11820, #10188, #14419, .T. ) ;
#1283=EDGE_LOOP ( 'NONE', ( #1748, #16988, #17522, #18628, #7883 ) ) ;
#1285=CARTESIAN_POINT ( 'NONE',  ( 3.333333333333335702, -2.694301256218268215, -3.300726591567084256 ) ) ;
#1327=CARTESIAN_POINT ( 'NONE',  ( -4.211140560182196957, -2.431303136016552013, -3.745885042887436178 ) ) ;
#1348=LINE ( 'NONE', #13249, #3675 ) ;
#1355=CARTESIAN_POINT ( 'NONE',  ( 4.000000000000000000, 1.680228229147133767, -3.316631783032546021 ) ) ;
#1422=CARTESIAN_POINT ( 'NONE',  ( 1.411581201560190495E-15, 4.862606272033091592, -3.745885042887436622 ) ) ;
#1442=CARTESIAN_POINT ( 'NONE',  ( 4.211405965630455661, 2.460463115436283932, -3.751298928144577882 ) ) ;
#1458=ORIENTED_EDGE ( 'NONE', *, *, #16123, .T. ) ;
#1460=( NAMED_UNIT ( * ) SI_UNIT ( $, .STERADIAN. ) SOLID_ANGLE_UNIT ( ) );
#1468=CARTESIAN_POINT ( 'NONE',  ( 0.000000000000000000, 0.000000000000000000, -5.000000000000000000 ) ) ;
#1482=B_SPLINE_CURVE_WITH_KNOTS ( 'NONE', 3,
 ( #9096, #15155, #16722, #12324, #18290, #3329, #12419, #1772 ),
 .UNSPECIFIED., .F., .F.,
 ( 4, 2, 2, 4 ),
 ( 0.005725059856848645212, 0.006314084072593634418, 0.006903108288338624492, 0.008081156719828603771 ),
 .UNSPECIFIED. ) ;
#1504=CARTESIAN_POINT ( 'NONE',  ( -4.000000000000003553, 2.309401076758496263, -3.504269196027868905 ) ) ;
#1522=CARTESIAN_POINT ( 'NONE',  ( -3.999999999999999112, -2.309401076758512694, -3.504269196027871125 ) ) ;
#1548=CARTESIAN_POINT ( 'NONE',  ( 4.000000000000000888, -0.8578082829538523635, -3.433262215449808696 ) ) ;
#1580=DIRECTION ( 'NONE',  ( 1.000000000000000000, 0.000000000000000000, 0.000000000000000000 ) ) ;
#1581=DIRECTION ( 'NONE',  ( 0.000000000000000000, 0.000000000000000000, -1.000000000000000000 ) ) ;
#1583=VERTEX_POINT ( 'NONE', #6296 ) ;
#1586=B_SPLINE_CURVE_WITH_KNOTS ( 'NONE', 3,
 ( #5604, #14854, #17510, #14461, #14556 ),
 .UNSPECIFIED., .F., .F.,
 ( 4, 1, 4 ),
 ( 0.000000000000000000, 0.002309401076758505356, 0.004618802153517010713 ),
 .UNSPECIFIED. ) ;
#1659=EDGE_LOOP ( 'NONE', ( #11246, #808 ) ) ;
#1666=CARTESIAN_POINT ( 'NONE',  ( -4.000000000000000000, 0.7924765000094600165, -0.05906175389889745803 ) ) ;
#1685=EDGE_LOOP ( 'NONE', ( #4885, #3401, #822, #4248, #3393, #10422, #9731 ) ) ;
#1686=CARTESIAN_POINT ( 'NONE',  ( -2.059999999999998721, 2.522772406243545965E-16, -0.3080913168122742518 ) ) ;
#1706=CARTESIAN_POINT ( 'NONE',  ( 8.673617379884035472E-16, 4.618802153517012954, -5.000000000000000000 ) ) ;
#1708=CARTESIAN_POINT ( 'NONE',  ( 1.144235203016666258, 3.958177651039090250, -0.09382832055445661235 ) ) ;
#1712=EDGE_CURVE ( 'NONE', #12416, #7197, #10347, .T. ) ;
#1721=CARTESIAN_POINT ( 'NONE',  ( -1.828356344711647319, -3.563200125723192002, -1.076197711133951296E-14 ) ) ;
#1729=FACE_OUTER_BOUND ( 'NONE', #16285, .T. ) ;
#1732=ORIENTED_EDGE ( 'NONE', *, *, #12259, .T. ) ;
#1748=ORIENTED_EDGE ( 'NONE', *, *, #5307, .T. ) ;
#1770=CARTESIAN_POINT ( 'NONE',  ( 0.000000000000000000, 0.000000000000000000, -4.974599999999998801 ) ) ;
#1772=CARTESIAN_POINT ( 'NONE',  ( 4.000000000000000000, 2.309401076758515803, -0.4999999999999995559 ) ) ;
#1785=CARTESIAN_POINT ( 'NONE',  ( 4.000000000000000000, -2.309401076758516691, -0.4999999999999995559 ) ) ;
#1792=DIRECTION ( 'NONE',  ( 0.000000000000000000, 0.000000000000000000, -1.000000000000000000 ) ) ;
#1808=DIRECTION ( 'NONE',  ( 0.000000000000000000, 0.000000000000000000, -1.000000000000000000 ) ) ;
#1869=CARTESIAN_POINT ( 'NONE',  ( 4.211140560182196957, 2.431303136016536470, -3.745885042887433514 ) ) ;
#1906=ORIENTED_EDGE ( 'NONE', *, *, #15604, .F. ) ;
#1915=CARTESIAN_POINT ( 'NONE',  ( -1.391697335622809950, -4.043246145443391448, -3.503898532754372575 ) ) ;
#1925=DIRECTION ( 'NONE',  ( -1.000000000000000000, 0.000000000000000000, 0.000000000000000000 ) ) ;
#1940=CARTESIAN_POINT ( 'NONE',  ( 4.101954839143203912, 2.368264730583012234, -3.681130640444374436 ) ) ;
#1948=CARTESIAN_POINT ( 'NONE',  ( -3.349226789952655547, -2.685125164760744809, -0.2236248678334863682 ) ) ;
#1960=DIRECTION ( 'NONE',  ( -0.8191520442889902442, 0.000000000000000000, -0.5735764363510482688 ) ) ;
#1965=DIRECTION ( 'NONE',  ( 1.000000000000000000, 0.000000000000000000, 0.000000000000000000 ) ) ;
#1966=UNCERTAINTY_MEASURE_WITH_UNIT (LENGTH_MEASURE( 1.000000000000000082E-05 ), #9972, 'distance_accuracy_value', 'NONE');
#1970=VERTEX_POINT ( 'NONE', #12154 ) ;
#2013=CARTESIAN_POINT ( 'NONE',  ( -2.804994570502171047, -3.229033611042465335, -3.526374918436838701 ) ) ;
#2049=DIRECTION ( 'NONE',  ( -0.000000000000000000, -0.000000000000000000, 1.000000000000000000 ) ) ;
#2059=CARTESIAN_POINT ( 'NONE',  ( 2.855764796983346177, -2.970025579236428737, -0.09382832055446485575 ) ) ;
#2079=ORIENTED_EDGE ( 'NONE', *, *, #8174, .T. ) ;
#2094=CARTESIAN_POINT ( 'NONE',  ( 0.000000000000000000, 0.000000000000000000, -0.3080913168122742518 ) ) ;
#2097=DIRECTION ( 'NONE',  ( 1.000000000000000000, 0.000000000000000000, 0.000000000000000000 ) ) ;
#2106=AXIS2_PLACEMENT_3D ( 'NONE', #14519, #11790, #4559 ) ;
#2110=CARTESIAN_POINT ( 'NONE',  ( -2.000000000000007550, -3.464101615137749945, 0.000000000000000000 ) ) ;
#2112=ADVANCED_FACE ( 'NONE', ( #9027 ), #3827, .T. ) ;
#2125=FACE_OUTER_BOUND ( 'NONE', #6248, .T. ) ;
#2132=CIRCLE ( 'NONE', #18054, 4.000000000000000000 ) ;
#2141=ORIENTED_EDGE ( 'NONE', *, *, #18816, .T. ) ;
#2167=CARTESIAN_POINT ( 'NONE',  ( 4.024499207728847949, -2.323545700935699454, -3.572172305156873673 ) ) ;
#2183=EDGE_CURVE ( 'NONE', #17562, #4492, #18603, .T. ) ;
#2184=CARTESIAN_POINT ( 'NONE',  ( 0.02448733951239481094, 4.877042772274728044, -3.751161874094022242 ) ) ;
#2250=CARTESIAN_POINT ( 'NONE',  ( 1.317756351988342622, -3.857995168970215438, -0.04852650426602527628 ) ) ;
#2251=DIRECTION ( 'NONE',  ( -0.000000000000000000, -0.000000000000000000, 1.000000000000000000 ) ) ;
#2259=DIRECTION ( 'NONE',  ( -1.000000000000000000, 0.000000000000000000, 0.000000000000000000 ) ) ;
#2262=CARTESIAN_POINT ( 'NONE',  ( -2.499999999999999556, 3.061616997868382648E-16, 3.469446951953614189E-15 ) ) ;
#2270=AXIS2_PLACEMENT_3D ( 'NONE', #18762, #2049, #11233 ) ;
#2275=FACE_OUTER_BOUND ( 'NONE', #5001, .T. ) ;
#2284=CARTESIAN_POINT ( 'NONE',  ( -2.742827927723112236, -3.035229711105190464, -3.433252694550595230 ) ) ;
#2298=FACE_OUTER_BOUND ( 'NONE', #2561, .T. ) ;
#2301=CARTESIAN_POINT ( 'NONE',  ( 1.747541505913279281, -3.837784562140273081, -3.503702292528912299 ) ) ;
#2317=ADVANCED_FACE ( 'NONE', ( #2275 ), #18527, .F. ) ;
#2323=ORIENTED_EDGE ( 'NONE', *, *, #16523, .F. ) ;
#2380=CARTESIAN_POINT ( 'NONE',  ( 0.1410422978106145031, -4.700232962125109104, -3.687027686973628704 ) ) ;
#2392=LINE ( 'NONE', #4154, #11487 ) ;
#2417=CIRCLE ( 'NONE', #4292, 4.000000000000000000 ) ;
#2534=ORIENTED_EDGE ( 'NONE', *, *, #15458, .F. ) ;
#2544=CARTESIAN_POINT ( 'NONE',  ( 2.000000000000008882, 3.464101615137749945, 0.000000000000000000 ) ) ;
#2561=EDGE_LOOP ( 'NONE', ( #3567, #17100, #10119, #4108 ) ) ;
#2592=CARTESIAN_POINT ( 'NONE',  ( 1.567478505476134606E-15, 4.618802153517012066, -3.433295621305382905 ) ) ;
#2607=FACE_OUTER_BOUND ( 'NONE', #15254, .T. ) ;
#2624=( NAMED_UNIT ( * ) PLANE_ANGLE_UNIT ( ) SI_UNIT ( $, .RADIAN. ) );
#2631=VECTOR ( 'NONE', #15371, 1000.000000000000000 ) ;
#2632=DIRECTION ( 'NONE',  ( 1.000000000000000000, 0.000000000000000000, 0.000000000000000000 ) ) ;
#2634=FACE_OUTER_BOUND ( 'NONE', #12321, .T. ) ;
#2648=EDGE_CURVE ( 'NONE', #13696, #4492, #3094, .T. ) ;
#2650=CARTESIAN_POINT ( 'NONE',  ( -1.243802165048909503, 3.900692638707381921, -3.223146290109805800 ) ) ;
#2668=EDGE_CURVE ( 'NONE', #6163, #15956, #5228, .T. ) ;
#2678=B_SPLINE_CURVE_WITH_KNOTS ( 'NONE', 3,
 ( #2834, #1183, #11537, #15, #17499, #11626 ),
 .UNSPECIFIED., .F., .F.,
 ( 4, 2, 4 ),
 ( 0.002452478801916376308, 0.003676905084148007850, 0.004901331366379639391 ),
 .UNSPECIFIED. ) ;
#2741=CARTESIAN_POINT ( 'NONE',  ( 2.500000000000000444, 0.000000000000000000, -5.000000000000000888 ) ) ;
#2747=AXIS2_PLACEMENT_3D ( 'NONE', #17009, #11044, #3328 ) ;
#2748=DIRECTION ( 'NONE',  ( 0.000000000000000000, 0.000000000000000000, -1.000000000000000000 ) ) ;
#2762=VERTEX_POINT ( 'NONE', #511 ) ;
#2793=CARTESIAN_POINT ( 'NONE',  ( 3.861362476283255685, 2.629030857715988656, -3.671615880910370500 ) ) ;
#2798=EDGE_CURVE ( 'NONE', #7197, #1583, #16448, .T. ) ;
#2808=CARTESIAN_POINT ( 'NONE',  ( 4.000000000000000000, 2.309401076758497151, -5.000000000000000000 ) ) ;
#2811=CARTESIAN_POINT ( 'NONE',  ( 4.000000000000000000, 0.8378280264232961239, -3.220590601395640018 ) ) ;
#2826=VERTEX_POINT ( 'NONE', #1869 ) ;
#2832=VERTEX_POINT ( 'NONE', #12322 ) ;
#2834=CARTESIAN_POINT ( 'NONE',  ( -4.197393957002303999, -7.773935952363655451E-14, -3.503767560748929810 ) ) ;
#2835=CARTESIAN_POINT ( 'NONE',  ( 4.207491450040567571, -2.029819825146485179, -3.671670828759567407 ) ) ;
#2922=CARTESIAN_POINT ( 'NONE',  ( 2.500000000000000444, 0.000000000000000000, -25.03750572909317285 ) ) ;
#2990=CARTESIAN_POINT ( 'NONE',  ( -1.655952806101422814, 3.662737355149034979, -7.623296525288699970E-18 ) ) ;
#3000=CIRCLE ( 'NONE', #6122, 2.500000000000000888 ) ;
#3035=CARTESIAN_POINT ( 'NONE',  ( 0.000000000000000000, 0.000000000000000000, 0.000000000000000000 ) ) ;
#3042=CARTESIAN_POINT ( 'NONE',  ( 2.682243648011666703, 3.070208061305304881, -0.04852650426601266831 ) ) ;
#3059=CONICAL_SURFACE ( 'NONE', #8682, 4.000000000000000000, 0.8911886515913786111 ) ;
#3090=EDGE_LOOP ( 'NONE', ( #6766, #11239, #12035, #5070 ) ) ;
#3094=B_SPLINE_CURVE_WITH_KNOTS ( 'NONE', 3,
 ( #12030, #13494, #3042, #18001, #5890, #7443 ),
 .UNSPECIFIED., .F., .F.,
 ( 4, 2, 4 ),
 ( 0.002365888236227995517, 0.003551327329835084114, 0.004736766423442172712 ),
 .UNSPECIFIED. ) ;
#3173=LINE ( 'NONE', #265, #18340 ) ;
#3224=DIRECTION ( 'NONE',  ( -0.000000000000000000, -0.000000000000000000, 1.000000000000000000 ) ) ;
#3237=B_SPLINE_CURVE_WITH_KNOTS ( 'NONE', 3,
 ( #16713, #18096, #4706, #13681, #15051, #3320 ),
 .UNSPECIFIED., .F., .F.,
 ( 4, 2, 4 ),
 ( 0.003358874760055551890, 0.004541967308452098118, 0.005725059856848645212 ),
 .UNSPECIFIED. ) ;
#3264=EDGE_CURVE ( 'NONE', #12007, #12136, #13344, .T. ) ;
#3276=AXIS2_PLACEMENT_3D ( 'NONE', #13544, #12281, #6041 ) ;
#3286=DIRECTION ( 'NONE',  ( 0.000000000000000000, 0.000000000000000000, -1.000000000000000000 ) ) ;
#3312=CARTESIAN_POINT ( 'NONE',  ( -4.000000000000000888, 1.563622288139195238, -0.2253451193528307472 ) ) ;
#3313=CARTESIAN_POINT ( 'NONE',  ( -1.149515148933674504E-15, -4.647091401871393579, -3.572172305156879890 ) ) ;
#3320=CARTESIAN_POINT ( 'NONE',  ( 4.000000000000000000, 0.000000000000000000, 0.000000000000000000 ) ) ;
#3328=DIRECTION ( 'NONE',  ( -1.000000000000000000, 0.000000000000000000, 0.000000000000000000 ) ) ;
#3329=CARTESIAN_POINT ( 'NONE',  ( 4.000000000000000888, 1.563622288139206118, -0.2253451193528334950 ) ) ;
#3339=CARTESIAN_POINT ( 'NONE',  ( -4.101948962586059011, 2.368261337751163875, -3.681124513963739187 ) ) ;
#3364=ADVANCED_FACE ( 'NONE', ( #7630 ), #18024, .F. ) ;
#3393=ORIENTED_EDGE ( 'NONE', *, *, #8869, .T. ) ;
#3401=ORIENTED_EDGE ( 'NONE', *, *, #10471, .T. ) ;
#3414=CARTESIAN_POINT ( 'NONE',  ( -4.000000000000000000, 1.941961291383472732, -0.3515519931180205448 ) ) ;
#3435=EDGE_LOOP ( 'NONE', ( #8036, #5423, #6861, #10062 ) ) ;
#3476=DIRECTION ( 'NONE',  ( 1.000000000000000000, 0.000000000000000000, 0.000000000000000000 ) ) ;
#3505=CARTESIAN_POINT ( 'NONE',  ( -4.000000000000000000, 2.309401076758498483, -0.4999999999999927280 ) ) ;
#3522=AXIS2_PLACEMENT_3D ( 'NONE', #3623, #5105, #6666 ) ;
#3540=CARTESIAN_POINT ( 'NONE',  ( -2.171643655288372443, 3.365003104552320767, 2.541098841762897165E-18 ) ) ;
#3567=ORIENTED_EDGE ( 'NONE', *, *, #9167, .F. ) ;
#3569=CARTESIAN_POINT ( 'NONE',  ( -2.688821387764050996E-14, -4.618802153517012954, -0.4999999999999995559 ) ) ;
#3572=CARTESIAN_POINT ( 'NONE',  ( -0.6448876103708541807, -4.246476118072358474, -0.2256878752776773356 ) ) ;
#3589=ORIENTED_EDGE ( 'NONE', *, *, #16423, .F. ) ;
#3603=VECTOR ( 'NONE', #7378, 1000.000000000000000 ) ;
#3620=CARTESIAN_POINT ( 'NONE',  ( 0.6507732100473444525, -4.243078065514795050, -0.2236248678334952777 ) ) ;
#3623=CARTESIAN_POINT ( 'NONE',  ( 0.000000000000000000, 0.000000000000000000, 0.000000000000000000 ) ) ;
#3625=EDGE_CURVE ( 'NONE', #10188, #1583, #9378, .T. ) ;
#3651=ORIENTED_EDGE ( 'NONE', *, *, #770, .F. ) ;
#3675=VECTOR ( 'NONE', #12368, 999.9999999999998863 ) ;
#3738=CARTESIAN_POINT ( 'NONE',  ( -0.5276280594146446346, 4.314175951381965746, -3.320322319201721495 ) ) ;
#3747=CARTESIAN_POINT ( 'NONE',  ( -4.000000000000000000, 0.000000000000000000, 0.000000000000000000 ) ) ;
#3784=EDGE_CURVE ( 'NONE', #15956, #12903, #8032, .T. ) ;
#3807=EDGE_LOOP ( 'NONE', ( #13200, #12509, #16817, #5093, #368, #10022 ) ) ;
#3827=CONICAL_SURFACE ( 'NONE', #8824, 5.560781378645573980, 1.221730476396046816 ) ;
#3828=DIRECTION ( 'NONE',  ( 0.000000000000000000, 0.000000000000000000, 1.000000000000000000 ) ) ;
#3832=CARTESIAN_POINT ( 'NONE',  ( -2.807080416178626692, 3.225969019225154444, -3.502507215260441065 ) ) ;
#3843=CARTESIAN_POINT ( 'NONE',  ( -3.540020015735593439, -2.810662092924100630, -3.602146406945814672 ) ) ;
#3858=CARTESIAN_POINT ( 'NONE',  ( -0.1750025118121544265, -4.719839900820635314, -3.469254087858253399 ) ) ;
#3867=CARTESIAN_POINT ( 'NONE',  ( 1.393927851585479161, -4.043713361053543842, -3.526374918436840922 ) ) ;
#3874=CARTESIAN_POINT ( 'NONE',  ( 2.100000000000000089, 0.000000000000000000, -4.694516984716113228 ) ) ;
#3911=ORIENTED_EDGE ( 'NONE', *, *, #908, .F. ) ;
#3928=AXIS2_PLACEMENT_3D ( 'NONE', #1133, #7279, #10315 ) ;
#3943=EDGE_CURVE ( 'NONE', #17562, #9205, #7011, .T. ) ;
#4068=CARTESIAN_POINT ( 'NONE',  ( 1.391697335622810172, 4.043246145443375461, -3.503898532754365913 ) ) ;
#4108=ORIENTED_EDGE ( 'NONE', *, *, #9892, .T. ) ;
#4114=CARTESIAN_POINT ( 'NONE',  ( -4.000000000000000000, -2.309401076758512694, -3.433295621305382461 ) ) ;
#4129=AXIS2_PLACEMENT_3D ( 'NONE', #1468, #16030, #2632 ) ;
#4154=CARTESIAN_POINT ( 'NONE',  ( 4.000000000000000000, -2.309401076758514915, -5.000000000000000000 ) ) ;
#4166=CARTESIAN_POINT ( 'NONE',  ( 2.804994570502171047, 3.229033611042449792, -3.526374918436834704 ) ) ;
#4167=CARTESIAN_POINT ( 'NONE',  ( 2.691179338796023329E-15, 4.647089433458991614, -3.572167766733753691 ) ) ;
#4196=SURFACE_SIDE_STYLE ('',( #13084 ) ) ;
#4222=ADVANCED_FACE ( 'NONE', ( #7828 ), #18659, .T. ) ;
#4224=EDGE_CURVE ( 'NONE', #6163, #16577, #10302, .T. ) ;
#4225=CARTESIAN_POINT ( 'NONE',  ( -3.522875095019672109, 2.820352903225427532, -3.598441714920591394 ) ) ;
#4248=ORIENTED_EDGE ( 'NONE', *, *, #13454, .F. ) ;
#4279=VERTEX_POINT ( 'NONE', #15645 ) ;
#4292=AXIS2_PLACEMENT_3D ( 'NONE', #15614, #12293, #6534 ) ;
#4347=DIRECTION ( 'NONE',  ( 1.000000000000000000, 0.000000000000000000, 0.000000000000000000 ) ) ;
#4355=ADVANCED_FACE ( 'NONE', ( #614 ), #12106, .T. ) ;
#4403=DIRECTION ( 'NONE',  ( 0.000000000000000000, 0.000000000000000000, 1.000000000000000000 ) ) ;
#4452=CARTESIAN_POINT ( 'NONE',  ( 1.567478505476134606E-15, 4.618802153517012066, -3.433295621305382905 ) ) ;
#4460=CIRCLE ( 'NONE', #16009, 2.500000000000000444 ) ;
#4481=CARTESIAN_POINT ( 'NONE',  ( -4.197393957002303999, -0.8151795401431414234, -3.503767560748935139 ) ) ;
#4492=VERTEX_POINT ( 'NONE', #4883 ) ;
#4496=ORIENTED_EDGE ( 'NONE', *, *, #10471, .F. ) ;
#4510=CARTESIAN_POINT ( 'NONE',  ( 4.175002511812151873, 2.208363329454889445, -3.469254087858244073 ) ) ;
#4511=CARTESIAN_POINT ( 'NONE',  ( 0.000000000000000000, 0.000000000000000000, 0.000000000000000000 ) ) ;
#4523=CARTESIAN_POINT ( 'NONE',  ( -4.000000000000000000, 2.309401076758498483, -3.433295621305379353 ) ) ;
#4559=DIRECTION ( 'NONE',  ( -1.000000000000000000, 0.000000000000000000, 0.000000000000000000 ) ) ;
#4565=CARTESIAN_POINT ( 'NONE',  ( 4.204115023516791005, -1.660442669500199919, -3.602151381774560068 ) ) ;
#4596=CARTESIAN_POINT ( 'NONE',  ( 1.567478505476134606E-15, 4.618802153517012066, -5.000000000000000000 ) ) ;
#4608=ADVANCED_FACE ( 'NONE', ( #874 ), #11480, .F. ) ;
#4613=CARTESIAN_POINT ( 'NONE',  ( 2.756197834950227410, 3.027510591568626896, -3.223146290109805356 ) ) ;
#4632=CIRCLE ( 'NONE', #13686, 5.384454397937118664 ) ;
#4635=B_SPLINE_CURVE_WITH_KNOTS ( 'NONE', 3,
 ( #11997, #7215, #4481, #5856 ),
 .UNSPECIFIED., .F., .F.,
 ( 4, 4 ),
 ( 0.000000000000000000, 0.002452478801916376308 ),
 .UNSPECIFIED. ) ;
#4652=CARTESIAN_POINT ( 'NONE',  ( 2.100000000000000089, 0.000000000000000000, -5.000000000000000000 ) ) ;
#4690=CARTESIAN_POINT ( 'NONE',  ( -4.000000000000000000, 1.700094919196744270, -3.320312364301766017 ) ) ;
#4695=ADVANCED_FACE ( 'NONE', ( #2607 ), #7435, .T. ) ;
#4700=DIRECTION ( 'NONE',  ( 0.5000000000000022204, 0.8660254037844374864, -0.000000000000000000 ) ) ;
#4706=CARTESIAN_POINT ( 'NONE',  ( 4.000000000000000000, -1.560351142792952617, -0.2242961665059816367 ) ) ;
#4712=CARTESIAN_POINT ( 'NONE',  ( -0.02511973781850462134, 4.877415612947412882, -3.751298745799839462 ) ) ;
#4718=ADVANCED_FACE ( 'NONE', ( #14620 ), #8665, .F. ) ;
#4785=ORIENTED_EDGE ( 'NONE', *, *, #11072, .T. ) ;
#4801=CARTESIAN_POINT ( 'NONE',  ( -6.259644161404860030E-16, -4.618802153517027165, -3.433295621305388234 ) ) ;
#4805=DIRECTION ( 'NONE',  ( -0.8660254037844377084, -0.5000000000000015543, 0.000000000000000000 ) ) ;
#4816=DIRECTION ( 'NONE',  ( -0.000000000000000000, 0.000000000000000000, -1.000000000000000000 ) ) ;
#4825=CARTESIAN_POINT ( 'NONE',  ( -4.154094228333542915, 2.398367420968061658, -3.721909803043254694 ) ) ;
#4862=CARTESIAN_POINT ( 'NONE',  ( -2.449848172108560540, -3.432307619358754724, -3.503702292528910078 ) ) ;
#4865=CARTESIAN_POINT ( 'NONE',  ( 0.000000000000000000, 0.000000000000000000, 0.000000000000000000 ) ) ;
#4883=CARTESIAN_POINT ( 'NONE',  ( 4.000000000000000000, 2.309401076758515803, -0.4999999999999995559 ) ) ;
#4885=ORIENTED_EDGE ( 'NONE', *, *, #13692, .T. ) ;
#4886=CARTESIAN_POINT ( 'NONE',  ( 3.999999999999999112, 2.309401076758497595, -3.504271511727124366 ) ) ;
#4889=ORIENTED_EDGE ( 'NONE', *, *, #18005, .T. ) ;
#4890=CARTESIAN_POINT ( 'NONE',  ( -4.000000000000000000, 0.000000000000000000, 0.000000000000000000 ) ) ;
#4926=EDGE_LOOP ( 'NONE', ( #12412, #9584, #5761, #15527 ) ) ;
#4961=EDGE_CURVE ( 'NONE', #16577, #15956, #10743, .T. ) ;
#4966=CARTESIAN_POINT ( 'NONE',  ( -4.175002511812151873, -2.208363329454905877, -3.469254087858246738 ) ) ;
#5001=EDGE_LOOP ( 'NONE', ( #8223, #18501, #18657, #11880 ) ) ;
#5019=CARTESIAN_POINT ( 'NONE',  ( -2.687328764639638656, 3.067272167851286202, -0.05923475698270370959 ) ) ;
#5021=DIRECTION ( 'NONE',  ( -1.000000000000000000, 0.000000000000000000, 0.000000000000000000 ) ) ;
#5070=ORIENTED_EDGE ( 'NONE', *, *, #9476, .F. ) ;
#5093=ORIENTED_EDGE ( 'NONE', *, *, #782, .F. ) ;
#5101=DIRECTION ( 'NONE',  ( -0.000000000000000000, -0.000000000000000000, 1.000000000000000000 ) ) ;
#5104=ORIENTED_EDGE ( 'NONE', *, *, #11016, .F. ) ;
#5105=DIRECTION ( 'NONE',  ( -0.000000000000000000, 0.000000000000000000, -1.000000000000000000 ) ) ;
#5110=CARTESIAN_POINT ( 'NONE',  ( -4.000000000000000000, -0.7890432684750890990, -0.04868663549882315533 ) ) ;
#5120=ORIENTED_EDGE ( 'NONE', *, *, #17523, .T. ) ;
#5144=B_SPLINE_CURVE_WITH_KNOTS ( 'NONE', 3,
 ( #1327, #16269, #19104, #5919, #1522, #6009 ),
 .UNSPECIFIED., .F., .F.,
 ( 4, 2, 4 ),
 ( -3.640115492409406142E-06, 0.0002066546034003385283, 0.0004169493222930864334 ),
 .UNSPECIFIED. ) ;
#5145=ORIENTED_EDGE ( 'NONE', *, *, #13454, .T. ) ;
#5154=PLANE ( 'NONE',  #10387 ) ;
#5194=CARTESIAN_POINT ( 'NONE',  ( -0.6937372685066653943, 4.453844082567723461, -3.610536846335889116 ) ) ;
#5213=LINE ( 'NONE', #17320, #871 ) ;
#5220=ADVANCED_FACE ( 'NONE', ( #2298 ), #8672, .F. ) ;
#5228=CIRCLE ( 'NONE', #7089, 4.000000000000000000 ) ;
#5233=DIRECTION ( 'NONE',  ( -0.000000000000000000, -0.000000000000000000, 1.000000000000000000 ) ) ;
#5241=CARTESIAN_POINT ( 'NONE',  ( 3.436319922986518449, -2.634841920959471562, -3.531542292954761741 ) ) ;
#5296=CARTESIAN_POINT ( 'NONE',  ( -2.805705207896067144, 3.226868319750155312, -3.503898532754364581 ) ) ;
#5307=EDGE_CURVE ( 'NONE', #2832, #15250, #5144, .T. ) ;
#5320=EDGE_CURVE ( 'NONE', #11379, #15041, #19205, .T. ) ;
#5326=EDGE_CURVE ( 'NONE', #11820, #7197, #14994, .T. ) ;
#5327=ORIENTED_EDGE ( 'NONE', *, *, #12139, .T. ) ;
#5332=DIRECTION ( 'NONE',  ( -1.000000000000000000, 0.000000000000000000, 0.000000000000000000 ) ) ;
#5394=CARTESIAN_POINT ( 'NONE',  ( -3.511755186886750479, 2.826662030176366081, -3.597382984111578086 ) ) ;
#5423=ORIENTED_EDGE ( 'NONE', *, *, #9703, .T. ) ;
#5426=VECTOR ( 'NONE', #9102, 999.9999999999998863 ) ;
#5458=CARTESIAN_POINT ( 'NONE',  ( 3.999999999999999112, -1.539600717839012978, -3.300726591567080703 ) ) ;
#5480=VECTOR ( 'NONE', #10167, 1000.000000000000000 ) ;
#5583=FILL_AREA_STYLE_COLOUR ( '', #9554 ) ;
#5591=CONICAL_SURFACE ( 'NONE', #11501, 5.560781378645573980, 1.221730476396046816 ) ;
#5592=CARTESIAN_POINT ( 'NONE',  ( 4.204015924366189871, -1.626724848190933548, -3.610627190413393084 ) ) ;
#5604=CARTESIAN_POINT ( 'NONE',  ( -4.000000000000000000, -2.309401076758512694, -3.433295621305382461 ) ) ;
#5639=CARTESIAN_POINT ( 'NONE',  ( 1.411581201560190495E-15, 4.862606272033091592, -3.745885042887436622 ) ) ;
#5640=DIRECTION ( 'NONE',  ( -1.000000000000000000, 0.000000000000000000, 0.000000000000000000 ) ) ;
#5669=ADVANCED_FACE ( 'NONE', ( #7615 ), #6793, .F. ) ;
#5693=EDGE_LOOP ( 'NONE', ( #573, #12918, #11844, #8837 ) ) ;
#5710=STYLED_ITEM('',(#19371),#7579);
#5724=AXIS2_PLACEMENT_3D ( 'NONE', #18737, #1139, #15893 ) ;
#5727=CARTESIAN_POINT ( 'NONE',  ( 2.500000000000000888, 3.061616997868384127E-16, -4.974599999999998801 ) ) ;
#5761=ORIENTED_EDGE ( 'NONE', *, *, #908, .T. ) ;
#5780=DIRECTION ( 'NONE',  ( -1.000000000000000000, 0.000000000000000000, 0.000000000000000000 ) ) ;
#5804=AXIS2_PLACEMENT_3D ( 'NONE', #2094, #16854, #8053 ) ;
#5856=CARTESIAN_POINT ( 'NONE',  ( -4.197393957002303999, -7.773935952363655451E-14, -3.503767560748929810 ) ) ;
#5867=AXIS2_PLACEMENT_3D ( 'NONE', #17608, #12825, #18790 ) ;
#5875=CARTESIAN_POINT ( 'NONE',  ( -6.259644161404859044E-16, -4.618802153517026277, -3.504271511727133248 ) ) ;
#5888=CARTESIAN_POINT ( 'NONE',  ( 4.140404888673277384, 2.228338276487440428, -3.686887068327033390 ) ) ;
#5890=CARTESIAN_POINT ( 'NONE',  ( 3.679171394226031122, 2.494631558665830973, -0.3503314178412474389 ) ) ;
#5897=VERTEX_POINT ( 'NONE', #16987 ) ;
#5919=CARTESIAN_POINT ( 'NONE',  ( -4.024497503033714452, -2.323544716729502468, -3.572167766733752803 ) ) ;
#5921=CARTESIAN_POINT ( 'NONE',  ( 0.000000000000000000, 0.000000000000000000, -5.000000000000000888 ) ) ;
#5941=CARTESIAN_POINT ( 'NONE',  ( 2.000000000000005329, -3.464101615137751722, 0.000000000000000000 ) ) ;
#5966=CARTESIAN_POINT ( 'NONE',  ( -4.211399284164270895, 2.459729995988205964, -3.751162237960538715 ) ) ;
#5974=FACE_OUTER_BOUND ( 'NONE', #12503, .T. ) ;
#5985=CYLINDRICAL_SURFACE ( 'NONE', #6628, 2.500000000000000444 ) ;
#5990=CARTESIAN_POINT ( 'NONE',  ( 1.567478505476134606E-15, 4.618802153517012066, -3.433295621305382905 ) ) ;
#6009=CARTESIAN_POINT ( 'NONE',  ( -4.000000000000000000, -2.309401076758512694, -3.433295621305382461 ) ) ;
#6016=DIRECTION ( 'NONE',  ( -1.000000000000000000, 0.000000000000000000, 0.000000000000000000 ) ) ;
#6027=DIRECTION ( 'NONE',  ( 1.000000000000000000, 0.000000000000000000, 0.000000000000000000 ) ) ;
#6039=CARTESIAN_POINT ( 'NONE',  ( 4.000000000000000888, 0.8228435280416209752, -3.430609588141487976 ) ) ;
#6041=DIRECTION ( 'NONE',  ( 0.000000000000000000, 0.000000000000000000, 1.000000000000000000 ) ) ;
#6064=CARTESIAN_POINT ( 'NONE',  ( -4.000000000000000000, 2.471528634177585282, -3.686887442155186712 ) ) ;
#6110=CIRCLE ( 'NONE', #510, 2.500000000000000444 ) ;
#6114=CARTESIAN_POINT ( 'NONE',  ( 1.734723475976807094E-15, 4.618802153517012954, -0.4999999999999995559 ) ) ;
#6122=AXIS2_PLACEMENT_3D ( 'NONE', #16856, #5233, #2097 ) ;
#6154=AXIS2_PLACEMENT_3D ( 'NONE', #11208, #13748, #1925 ) ;
#6155=ADVANCED_FACE ( 'NONE', ( #13158 ), #14876, .F. ) ;
#6161=CARTESIAN_POINT ( 'NONE',  ( -4.000000000000000000, 1.677772373332757194, -3.535253723897187506 ) ) ;
#6163=VERTEX_POINT ( 'NONE', #5941 ) ;
#6179=CARTESIAN_POINT ( 'NONE',  ( 2.742827927723449299, 3.035229711104609596, -3.433252694550591233 ) ) ;
#6186=CONICAL_SURFACE ( 'NONE', #18040, 4.000000000000000000, 0.8911886515913786111 ) ;
#6248=EDGE_LOOP ( 'NONE', ( #3589, #9100, #12186, #9265, #18364 ) ) ;
#6270=DIRECTION ( 'NONE',  ( 0.000000000000000000, 0.000000000000000000, -1.000000000000000000 ) ) ;
#6279=DIRECTION ( 'NONE',  ( 1.000000000000000000, 0.000000000000000000, 0.000000000000000000 ) ) ;
#6296=CARTESIAN_POINT ( 'NONE',  ( -2.500000000000000888, 0.000000000000000000, -4.974599999999998801 ) ) ;
#6306=FACE_OUTER_BOUND ( 'NONE', #1659, .T. ) ;
#6318=ORIENTED_EDGE ( 'NONE', *, *, #1048, .F. ) ;
#6323=AXIS2_PLACEMENT_3D ( 'NONE', #18280, #13484, #9182 ) ;
#6356=CARTESIAN_POINT ( 'NONE',  ( -2.000000000000007550, -3.464101615137749945, 0.000000000000000000 ) ) ;
#6413=CIRCLE ( 'NONE', #15140, 2.499999999999999556 ) ;
#6417=EDGE_CURVE ( 'NONE', #9031, #9797, #12064, .T. ) ;
#6443=ORIENTED_EDGE ( 'NONE', *, *, #9010, .F. ) ;
#6466=CARTESIAN_POINT ( 'NONE',  ( 0.000000000000000000, 0.000000000000000000, 0.000000000000000000 ) ) ;
#6478=CARTESIAN_POINT ( 'NONE',  ( -3.355112389629170799, 2.681727112203152963, -0.2256878752776689534 ) ) ;
#6488=ADVANCED_FACE ( 'NONE', ( #17261 ), #16964, .F. ) ;
#6509=VECTOR ( 'NONE', #17930, 1000.000000000000114 ) ;
#6522=CARTESIAN_POINT ( 'NONE',  ( 3.511755186886750923, -2.826662030176382956, -3.597382984111582083 ) ) ;
#6534=DIRECTION ( 'NONE',  ( 1.000000000000000000, 0.000000000000000000, 0.000000000000000000 ) ) ;
#6558=ORIENTED_EDGE ( 'NONE', *, *, #161, .T. ) ;
#6571=CARTESIAN_POINT ( 'NONE',  ( -5.560781378645575757, 6.809993116116508640E-16, -4.000000000000000000 ) ) ;
#6590=VERTEX_POINT ( 'NONE', #1422 ) ;
#6600=FACE_OUTER_BOUND ( 'NONE', #16430, .T. ) ;
#6628=AXIS2_PLACEMENT_3D ( 'NONE', #35, #11937, #17908 ) ;
#6666=DIRECTION ( 'NONE',  ( -1.000000000000000000, 0.000000000000000000, 0.000000000000000000 ) ) ;
#6667=CARTESIAN_POINT ( 'NONE',  ( 4.000000000000000000, -2.309401076758514915, -3.433295621305383349 ) ) ;
#6690=ORIENTED_EDGE ( 'NONE', *, *, #2648, .F. ) ;
#6716=CARTESIAN_POINT ( 'NONE',  ( 3.383466608491643077E-15, 4.736522675502341073, -3.681124513963742739 ) ) ;
#6734=ORIENTED_EDGE ( 'NONE', *, *, #13692, .F. ) ;
#6766=ORIENTED_EDGE ( 'NONE', *, *, #12697, .T. ) ;
#6793=( BOUNDED_SURFACE ( )  B_SPLINE_SURFACE ( 3, 2, ( 
 ( #308, #6064, #5966 ),
 ( #4690, #6161, #15136 ),
 ( #16321, #11914, #17887 ),
 ( #13279, #10640, #14946 ),
 ( #17983, #10449, #16607 ),
 ( #16513, #17791, #16229 ) ),
 .UNSPECIFIED., .F., .F., .F. ) 
 B_SPLINE_SURFACE_WITH_KNOTS ( ( 4, 2, 4 ),
 ( 3, 3 ),
 ( 0.02027752710269158445, 0.02273781595091097299, 0.02519810479913036153 ),
 ( 0.000000000000000000, 1.000000000000000000 ),
 .UNSPECIFIED. ) 
 GEOMETRIC_REPRESENTATION_ITEM ( )  RATIONAL_B_SPLINE_SURFACE ( (
 ( 1.000000000000000000, 0.8047781431712808242, 1.000000000000000000),
 ( 1.000000000000000000, 0.8123773247083928561, 1.000000000000000000),
 ( 1.000000000000000000, 0.8190670192154906326, 1.000000000000000000),
 ( 1.000000000000000000, 0.8192353552912178261, 1.000000000000000000),
 ( 1.000000000000000000, 0.8126132098226825917, 1.000000000000000000),
 ( 1.000000000000000000, 0.8047712465856394770, 1.000000000000000000) ) ) 
 REPRESENTATION_ITEM ( '' )  SURFACE ( )  );
#6796=AXIS2_PLACEMENT_3D ( 'NONE', #1770, #7730, #6279 ) ;
#6822=FACE_OUTER_BOUND ( 'NONE', #18291, .T. ) ;
#6861=ORIENTED_EDGE ( 'NONE', *, *, #12119, .T. ) ;
#6911=B_SPLINE_CURVE_WITH_KNOTS ( 'NONE', 3,
 ( #5639, #1047, #4068, #7000, #4166, #18734, #2793, #12953 ),
 .UNSPECIFIED., .F., .F.,
 ( 4, 2, 2, 4 ),
 ( 7.780516681398759253E-20, 0.002450665683189819696, 0.003675998524784729327, 0.004901331366379639391 ),
 .UNSPECIFIED. ) ;
#6916=CARTESIAN_POINT ( 'NONE',  ( 4.000000000000000000, 2.309401076758497151, -3.433295621305379353 ) ) ;
#6962=APPLICATION_CONTEXT ( 'automotive_design' ) ;
#6963=DIRECTION ( 'NONE',  ( 0.000000000000000000, 0.000000000000000000, -1.000000000000000000 ) ) ;
#7000=CARTESIAN_POINT ( 'NONE',  ( 2.449848172108560096, 3.432307619358740514, -3.503702292528905637 ) ) ;
#7004=CARTESIAN_POINT ( 'NONE',  ( 4.000000000000000000, -1.084202172485504434E-14, -3.142992957459231906 ) ) ;
#7011=B_SPLINE_CURVE_WITH_KNOTS ( 'NONE', 3,
 ( #8426, #7249, #10091, #17427, #11743 ),
 .UNSPECIFIED., .F., .F.,
 ( 4, 1, 4 ),
 ( 0.000000000000000000, 0.002309401076758505356, 0.004618802153517010713 ),
 .UNSPECIFIED. ) ;
#7050=B_SPLINE_CURVE_WITH_KNOTS ( 'NONE', 3,
 ( #17551, #14319, #6716, #4167, #958, #2592 ),
 .UNSPECIFIED., .F., .F.,
 ( 4, 2, 4 ),
 ( -3.640115492407174633E-06, 0.0002066546034003413743, 0.0004169493222930899571 ),
 .UNSPECIFIED. ) ;
#7058=CARTESIAN_POINT ( 'NONE',  ( -1.360585162435467455, 4.061296242128285883, -3.505054077164959203 ) ) ;
#7089=AXIS2_PLACEMENT_3D ( 'NONE', #4511, #18386, #13870 ) ;
#7110=AXIS2_PLACEMENT_3D ( 'NONE', #26, #1581, #13393 ) ;
#7150=( NAMED_UNIT ( * ) SI_UNIT ( $, .STERADIAN. ) SOLID_ANGLE_UNIT ( ) );
#7168=EDGE_CURVE ( 'NONE', #15956, #10850, #10197, .T. ) ;
#7197=VERTEX_POINT ( 'NONE', #9565 ) ;
#7215=CARTESIAN_POINT ( 'NONE',  ( -4.203833317240879275, -1.627343821129593859, -3.597273115243890818 ) ) ;
#7232=CARTESIAN_POINT ( 'NONE',  ( 0.000000000000000000, 0.000000000000000000, -5.000000000000000000 ) ) ;
#7249=CARTESIAN_POINT ( 'NONE',  ( 3.333333333333332593, 2.694301256218250007, -3.300726591567078483 ) ) ;
#7276=ORIENTED_EDGE ( 'NONE', *, *, #17283, .F. ) ;
#7279=DIRECTION ( 'NONE',  ( -0.000000000000000000, -0.000000000000000000, 1.000000000000000000 ) ) ;
#7298=CARTESIAN_POINT ( 'NONE',  ( 3.999999999999998224, 2.472263674411418588, -3.687027874309861897 ) ) ;
#7328=LINE ( 'NONE', #4596, #5480 ) ;
#7341=CARTESIAN_POINT ( 'NONE',  ( 0.000000000000000000, 0.000000000000000000, 0.000000000000000000 ) ) ;
#7373=ORIENTED_EDGE ( 'NONE', *, *, #9892, .F. ) ;
#7376=CARTESIAN_POINT ( 'NONE',  ( 5.560781378645573980, 6.809993116116507654E-16, -4.000000000000000000 ) ) ;
#7378=DIRECTION ( 'NONE',  ( 0.000000000000000000, 0.000000000000000000, 1.000000000000000000 ) ) ;
#7394=ORIENTED_EDGE ( 'NONE', *, *, #10539, .T. ) ;
#7435=CONICAL_SURFACE ( 'NONE', #16172, 4.000000000000000000, 0.8911886515913786111 ) ;
#7443=CARTESIAN_POINT ( 'NONE',  ( 4.000000000000000000, 2.309401076758515803, -0.4999999999999995559 ) ) ;
#7466=ORIENTED_EDGE ( 'NONE', *, *, #12259, .F. ) ;
#7472=ORIENTED_EDGE ( 'NONE', *, *, #3625, .T. ) ;
#7478=EDGE_CURVE ( 'NONE', #15041, #11485, #9466, .T. ) ;
#7553=AXIS2_PLACEMENT_3D ( 'NONE', #6466, #4816, #7732 ) ;
#7579=MANIFOLD_SOLID_BREP ( 'EndChamfer', #15382 ) ;
#7592=FACE_OUTER_BOUND ( 'NONE', #11787, .T. ) ;
#7615=FACE_OUTER_BOUND ( 'NONE', #1283, .T. ) ;
#7630=FACE_OUTER_BOUND ( 'NONE', #15315, .T. ) ;
#7652=CARTESIAN_POINT ( 'NONE',  ( 0.000000000000000000, 0.000000000000000000, -4.000000000000000000 ) ) ;
#7662=ADVANCED_FACE ( 'NONE', ( #12212 ), #8891, .T. ) ;
#7663=CARTESIAN_POINT ( 'NONE',  ( 1.312671235360372224, 3.860931062424219462, -0.05923475698270440348 ) ) ;
#7674=LINE ( 'NONE', #16287, #14569 ) ;
#7686=CARTESIAN_POINT ( 'NONE',  ( -1.274258131565027874, -3.883108878240886241, -3.220599429844051009 ) ) ;
#7702=( LENGTH_UNIT ( ) NAMED_UNIT ( * ) SI_UNIT ( .MILLI., .METRE. ) );
#7721=ADVANCED_FACE ( 'NONE', ( #5974 ), #17798, .T. ) ;
#7730=DIRECTION ( 'NONE',  ( -0.000000000000000000, -0.000000000000000000, 1.000000000000000000 ) ) ;
#7732=DIRECTION ( 'NONE',  ( -1.000000000000000000, 0.000000000000000000, 0.000000000000000000 ) ) ;
#7756=DIRECTION ( 'NONE',  ( -1.000000000000000000, 0.000000000000000000, 0.000000000000000000 ) ) ;
#7774=B_SPLINE_CURVE_WITH_KNOTS ( 'NONE', 3,
 ( #803, #5394, #5296, #14262, #10949, #5194, #900, #9877 ),
 .UNSPECIFIED., .F., .F.,
 ( 4, 2, 2, 4 ),
 ( 0.000000000000000000, 0.002450665683189820997, 0.003675998524784731495, 0.004901331366379641993 ),
 .UNSPECIFIED. ) ;
#7780=CARTESIAN_POINT ( 'NONE',  ( -0.3198814748697807464, -4.434118497892185040, -0.3507732604232532969 ) ) ;
#7823=EDGE_LOOP ( 'NONE', ( #2534, #8098, #18404, #14596 ) ) ;
#7828=FACE_OUTER_BOUND ( 'NONE', #11916, .T. ) ;
#7874=CARTESIAN_POINT ( 'NONE',  ( -1.144235203016679359, -3.958177651039096911, -0.09382832055446428676 ) ) ;
#7883=ORIENTED_EDGE ( 'NONE', *, *, #17523, .F. ) ;
#7906=CARTESIAN_POINT ( 'NONE',  ( -3.679171394226034675, -2.494631558665844739, -0.3503314178412558211 ) ) ;
#7977=EDGE_CURVE ( 'NONE', #17634, #12136, #14744, .T. ) ;
#8013=ORIENTED_EDGE ( 'NONE', *, *, #16891, .F. ) ;
#8017=CARTESIAN_POINT ( 'NONE',  ( 2.687328764639642653, -3.067272167851299969, -0.05923475698271395140 ) ) ;
#8032=CIRCLE ( 'NONE', #2106, 4.000000000000000000 ) ;
#8036=ORIENTED_EDGE ( 'NONE', *, *, #10539, .F. ) ;
#8053=DIRECTION ( 'NONE',  ( 1.000000000000000000, 0.000000000000000000, 0.000000000000000000 ) ) ;
#8098=ORIENTED_EDGE ( 'NONE', *, *, #1251, .F. ) ;
#8122=CARTESIAN_POINT ( 'NONE',  ( 1.734723475976807094E-15, 4.618802153517012954, -0.4999999999999995559 ) ) ;
#8123=CARTESIAN_POINT ( 'NONE',  ( 4.101954839143203912, -2.368264730583031330, -3.681130640444377988 ) ) ;
#8128=CARTESIAN_POINT ( 'NONE',  ( -4.000000000000000000, -1.560351142792950618, -0.2242961665059814425 ) ) ;
#8156=ADVANCED_FACE ( 'NONE', ( #2125 ), #5154, .T. ) ;
#8174=EDGE_CURVE ( 'NONE', #12416, #13022, #4460, .T. ) ;
#8179=DIRECTION ( 'NONE',  ( 0.5000000000000013323, -0.8660254037844379305, 0.000000000000000000 ) ) ;
#8195=ORIENTED_EDGE ( 'NONE', *, *, #10124, .T. ) ;
#8221=CARTESIAN_POINT ( 'NONE',  ( 0.000000000000000000, 0.000000000000000000, -4.484454397937119197 ) ) ;
#8223=ORIENTED_EDGE ( 'NONE', *, *, #13405, .T. ) ;
#8237=ORIENTED_EDGE ( 'NONE', *, *, #3625, .F. ) ;
#8239=CARTESIAN_POINT ( 'NONE',  ( -0.5469614295416921346, 4.303013824936271270, -3.535263753543735454 ) ) ;
#8248=CARTESIAN_POINT ( 'NONE',  ( 0.02511973781850649831, -4.877415612947427981, -3.751298745799844792 ) ) ;
#8258=CARTESIAN_POINT ( 'NONE',  ( 1.257172072275274388, -3.892973519170983110, -3.433252694550781303 ) ) ;
#8263=CARTESIAN_POINT ( 'NONE',  ( 0.000000000000000000, 0.000000000000000000, -0.3080913168122742518 ) ) ;
#8267=CARTESIAN_POINT ( 'NONE',  ( 0.6937372685066666156, -4.453844082567737672, -3.610536846335894445 ) ) ;
#8310=CARTESIAN_POINT ( 'NONE',  ( 2.171643655288379993, -3.365003104552334978, -1.195831703456429434E-14 ) ) ;
#8314=EDGE_LOOP ( 'NONE', ( #230, #4785, #9051, #18449, #16250 ) ) ;
#8321=LINE ( 'NONE', #11252, #582 ) ;
#8344=CIRCLE ( 'NONE', #13948, 0.5155456020628804703 ) ;
#8354=DIRECTION ( 'NONE',  ( 0.000000000000000000, 0.000000000000000000, 1.000000000000000000 ) ) ;
#8370=CARTESIAN_POINT ( 'NONE',  ( 4.000000000000000888, 1.539600717838996990, -3.300726591567079815 ) ) ;
#8371=ADVANCED_FACE ( 'NONE', ( #6822 ), #14320, .T. ) ;
#8424=PRODUCT ( 'hex flange nut gradea_iso_ISO - 4161 - M5 - N', 'hex flange nut gradea_iso_ISO - 4161 - M5 - N', '', ( #12673 ) ) ;
#8426=CARTESIAN_POINT ( 'NONE',  ( 4.000000000000000000, 2.309401076758497151, -3.433295621305379353 ) ) ;
#8459=CARTESIAN_POINT ( 'NONE',  ( 4.000000000000000000, -2.309401076758514915, -3.433295621305383349 ) ) ;
#8495=ORIENTED_EDGE ( 'NONE', *, *, #10124, .F. ) ;
#8507=( LENGTH_UNIT ( ) NAMED_UNIT ( * ) SI_UNIT ( .MILLI., .METRE. ) );
#8525=ORIENTED_EDGE ( 'NONE', *, *, #16123, .F. ) ;
#8581=PRODUCT_DEFINITION_SHAPE ( 'NONE', 'NONE',  #14778 ) ;
#8595=VECTOR ( 'NONE', #13135, 1000.000000000000227 ) ;
#8598=DIRECTION ( 'NONE',  ( 1.000000000000000000, 0.000000000000000000, 0.000000000000000000 ) ) ;
#8600=CARTESIAN_POINT ( 'NONE',  ( -4.000000000000000000, -7.806255641895631925E-15, -3.142992957459232350 ) ) ;
#8614=CARTESIAN_POINT ( 'NONE',  ( -1.257172072275743346, 3.892973519171203378, -3.433252694550776862 ) ) ;
#8651=EDGE_CURVE ( 'NONE', #12903, #11485, #13809, .T. ) ;
#8656=FACE_OUTER_BOUND ( 'NONE', #9072, .T. ) ;
#8662=AXIS2_PLACEMENT_3D ( 'NONE', #7652, #19200, #4347 ) ;
#8665=PLANE ( 'NONE',  #16476 ) ;
#8672=CONICAL_SURFACE ( 'NONE', #266, 2.059999999999998721, 0.9599310885968738161 ) ;
#8682=AXIS2_PLACEMENT_3D ( 'NONE', #4865, #3286, #5332 ) ;
#8690=PRESENTATION_STYLE_ASSIGNMENT (( #16120 ) ) ;
#8694=VERTEX_POINT ( 'NONE', #8122 ) ;
#8712=CARTESIAN_POINT ( 'NONE',  ( -4.175648173966055587, 2.207990556236529844, -3.469390959564062626 ) ) ;
#8758=CARTESIAN_POINT ( 'NONE',  ( -0.3208286057739654917, 4.433571671609680465, -0.3503314178412548774 ) ) ;
#8808=AXIS2_PLACEMENT_3D ( 'NONE', #8992, #4700, #18182 ) ;
#8824=AXIS2_PLACEMENT_3D ( 'NONE', #14988, #1792, #7756 ) ;
#8837=ORIENTED_EDGE ( 'NONE', *, *, #2798, .T. ) ;
#8838=DIRECTION ( 'NONE',  ( 0.000000000000000000, 0.000000000000000000, 1.000000000000000000 ) ) ;
#8858=ORIENTED_EDGE ( 'NONE', *, *, #4224, .F. ) ;
#8869=EDGE_CURVE ( 'NONE', #11219, #14097, #2678, .T. ) ;
#8884=CARTESIAN_POINT ( 'NONE',  ( 4.198928548860774157, -0.8158838809860124996, -3.526471437616918170 ) ) ;
#8891=PLANE ( 'NONE',  #12242 ) ;
#8910=B_SPLINE_CURVE_WITH_KNOTS ( 'NONE', 3,
 ( #11449, #911, #17413, #15942 ),
 .UNSPECIFIED., .F., .F.,
 ( 4, 4 ),
 ( 0.000000000000000000, 0.002452478801916361129 ),
 .UNSPECIFIED. ) ;
#8962=B_SPLINE_CURVE_WITH_KNOTS ( 'NONE', 3,
 ( #6667, #9587, #2167, #8123, #12611, #18584 ),
 .UNSPECIFIED., .F., .F.,
 ( 4, 2, 4 ),
 ( 4.336808689942017736E-19, 0.0002095117440864781224, 0.0004190234881729558111 ),
 .UNSPECIFIED. ) ;
#8992=CARTESIAN_POINT ( 'NONE',  ( 4.000000000000000000, 2.309401076758497151, -5.000000000000000000 ) ) ;
#8996=DIRECTION ( 'NONE',  ( -1.000000000000000000, 0.000000000000000000, 0.000000000000000000 ) ) ;
#9010=EDGE_CURVE ( 'NONE', #17562, #2826, #17597, .T. ) ;
#9020=ADVANCED_BREP_SHAPE_REPRESENTATION ( '', ( #7579, #10540 ), #17049 ) ;
#9027=FACE_OUTER_BOUND ( 'NONE', #18554, .T. ) ;
#9031=VERTEX_POINT ( 'NONE', #13851 ) ;
#9047=CARTESIAN_POINT ( 'NONE',  ( -0.6507732100473471171, 4.243078065514775510, -0.2236248678334823436 ) ) ;
#9051=ORIENTED_EDGE ( 'NONE', *, *, #5320, .T. ) ;
#9072=EDGE_LOOP ( 'NONE', ( #10952, #2141, #1458, #8013 ) ) ;
#9092=CARTESIAN_POINT ( 'NONE',  ( 1.274258131564866448, 3.883108878240963513, -3.220599429844046568 ) ) ;
#9096=CARTESIAN_POINT ( 'NONE',  ( 4.000000000000000000, 0.000000000000000000, 0.000000000000000000 ) ) ;
#9100=ORIENTED_EDGE ( 'NONE', *, *, #9476, .T. ) ;
#9102=DIRECTION ( 'NONE',  ( -0.8191520442889875797, 1.003171929053519570E-16, 0.5735764363510522656 ) ) ;
#9111=AXIS2_PLACEMENT_3D ( 'NONE', #12706, #2251, #11339 ) ;
#9129=CARTESIAN_POINT ( 'NONE',  ( 0.3198814748697593746, 4.434118497892183264, -0.3507732604232499107 ) ) ;
#9143=CARTESIAN_POINT ( 'NONE',  ( -1.654252653721913102, -3.663718938583024443, -0.01223254789874440342 ) ) ;
#9150=CARTESIAN_POINT ( 'NONE',  ( -3.472371940586054251, -2.614027278893156669, -3.320322319202162031 ) ) ;
#9167=EDGE_CURVE ( 'NONE', #1970, #13473, #16542, .T. ) ;
#9182=DIRECTION ( 'NONE',  ( 1.000000000000000000, 0.000000000000000000, 0.000000000000000000 ) ) ;
#9205=VERTEX_POINT ( 'NONE', #5990 ) ;
#9250=CARTESIAN_POINT ( 'NONE',  ( 0.000000000000000000, 0.000000000000000000, -5.000000000000000888 ) ) ;
#9265=ORIENTED_EDGE ( 'NONE', *, *, #1048, .T. ) ;
#9291=CONICAL_SURFACE ( 'NONE', #12422, 4.000000000000000000, 0.8911886515913786111 ) ;
#9318=FACE_BOUND ( 'NONE', #12305, .T. ) ;
#9353=ORIENTED_EDGE ( 'NONE', *, *, #782, .T. ) ;
#9378=LINE ( 'NONE', #15344, #13646 ) ;
#9379=ORIENTED_EDGE ( 'NONE', *, *, #11272, .T. ) ;
#9386=ORIENTED_EDGE ( 'NONE', *, *, #3943, .F. ) ;
#9391=CARTESIAN_POINT ( 'NONE',  ( -4.000000000000000000, -0.3979232138631226823, -3.896351557369779711E-17 ) ) ;
#9464=DIRECTION ( 'NONE',  ( -0.000000000000000000, -0.000000000000000000, 1.000000000000000000 ) ) ;
#9466=B_SPLINE_CURVE_WITH_KNOTS ( 'NONE', 3,
 ( #12334, #722, #6478, #10865, #5019, #16929, #3540, #9495 ),
 .UNSPECIFIED., .F., .F.,
 ( 4, 2, 2, 4 ),
 ( 2.465131517071352357E-07, 0.001183067374689843057, 0.001774477805458910071, 0.002365888236227977302 ),
 .UNSPECIFIED. ) ;
#9472=DIRECTION ( 'NONE',  ( 1.224646799147353207E-16, 1.000000000000000000, 0.000000000000000000 ) ) ;
#9476=EDGE_CURVE ( 'NONE', #4279, #11737, #12464, .T. ) ;
#9491=EDGE_CURVE ( 'NONE', #9205, #8694, #7328, .T. ) ;
#9495=CARTESIAN_POINT ( 'NONE',  ( -2.000000000000006661, 3.464101615137750834, 0.000000000000000000 ) ) ;
#9511=ORIENTED_EDGE ( 'NONE', *, *, #16891, .T. ) ;
#9516=VECTOR ( 'NONE', #9464, 1000.000000000000000 ) ;
#9518=ADVANCED_FACE ( 'NONE', ( #2634 ), #19256, .F. ) ;
#9532=CARTESIAN_POINT ( 'NONE',  ( -1.312671235360383548, -3.860931062424228788, -0.05923475698271369466 ) ) ;
#9554=COLOUR_RGB ( '',1.000000000000000000, 0.9490196078431372140, 0.9098039215686274384 ) ;
#9558=ORIENTED_EDGE ( 'NONE', *, *, #178, .T. ) ;
#9565=CARTESIAN_POINT ( 'NONE',  ( 2.500000000000000888, 3.061616997868384127E-16, -4.974599999999998801 ) ) ;
#9583=CARTESIAN_POINT ( 'NONE',  ( 2.345747346278113987, -3.264484291692503870, -0.01223254789874484924 ) ) ;
#9584=ORIENTED_EDGE ( 'NONE', *, *, #9167, .T. ) ;
#9587=CARTESIAN_POINT ( 'NONE',  ( 4.000000000000003553, -2.309401076758513138, -3.504271511727127031 ) ) ;
#9608=CARTESIAN_POINT ( 'NONE',  ( 0.1404048886732821022, 4.699864953788070565, -3.686887068327037387 ) ) ;
#9640=EDGE_CURVE ( 'NONE', #12903, #15041, #16457, .T. ) ;
#9663=ORIENTED_EDGE ( 'NONE', *, *, #9010, .T. ) ;
#9681=ORIENTED_EDGE ( 'NONE', *, *, #17331, .F. ) ;
#9703=EDGE_CURVE ( 'NONE', #13022, #1583, #18371, .T. ) ;
#9731=ORIENTED_EDGE ( 'NONE', *, *, #11016, .T. ) ;
#9777=ORIENTED_EDGE ( 'NONE', *, *, #15604, .T. ) ;
#9797=VERTEX_POINT ( 'NONE', #18175 ) ;
#9821=CARTESIAN_POINT ( 'NONE',  ( 2.712762565639649015, -3.052587955997662306, -3.430618716626630871 ) ) ;
#9877=CARTESIAN_POINT ( 'NONE',  ( 1.411581201560190495E-15, 4.862606272033091592, -3.745885042887436622 ) ) ;
#9892=EDGE_CURVE ( 'NONE', #10972, #13473, #6413, .T. ) ;
#9923=CARTESIAN_POINT ( 'NONE',  ( 3.522875095019493141, -2.820352903225631369, -3.598441714920572299 ) ) ;
#9972=( LENGTH_UNIT ( ) NAMED_UNIT ( * ) SI_UNIT ( .MILLI., .METRE. ) );
#10022=ORIENTED_EDGE ( 'NONE', *, *, #14007, .F. ) ;
#10037=ADVANCED_FACE ( 'NONE', ( #7592 ), #10714, .T. ) ;
#10062=ORIENTED_EDGE ( 'NONE', *, *, #1712, .F. ) ;
#10091=CARTESIAN_POINT ( 'NONE',  ( 2.000000000000000444, 3.464101615137754830, -3.142992957459231018 ) ) ;
#10119=ORIENTED_EDGE ( 'NONE', *, *, #16544, .T. ) ;
#10124=EDGE_CURVE ( 'NONE', #9797, #2832, #19223, .T. ) ;
#10125=CARTESIAN_POINT ( 'NONE',  ( 2.499999999999999556, 0.000000000000000000, 3.469446951953614189E-15 ) ) ;
#10167=DIRECTION ( 'NONE',  ( 0.000000000000000000, 0.000000000000000000, 1.000000000000000000 ) ) ;
#10181=CARTESIAN_POINT ( 'NONE',  ( -4.236525694536558362, 2.416953475386465211, -3.751298745799836354 ) ) ;
#10188=VERTEX_POINT ( 'NONE', #665 ) ;
#10197=B_SPLINE_CURVE_WITH_KNOTS ( 'NONE', 3,
 ( #6356, #18275, #12404, #1948, #7906, #499 ),
 .UNSPECIFIED., .F., .F.,
 ( 4, 2, 4 ),
 ( 0.002365888236228001588, 0.003551327329835089319, 0.004736766423442177049 ),
 .UNSPECIFIED. ) ;
#10241=CARTESIAN_POINT ( 'NONE',  ( 4.197478902586992966, -0.8524102783748346290, -3.505063281295504041 ) ) ;
#10253=CARTESIAN_POINT ( 'NONE',  ( 0.000000000000000000, 0.000000000000000000, 0.000000000000000000 ) ) ;
#10266=AXIS2_PLACEMENT_3D ( 'NONE', #3035, #6270, #8996 ) ;
#10302=B_SPLINE_CURVE_WITH_KNOTS ( 'NONE', 3,
 ( #425, #18289, #2250, #3620, #709, #12323 ),
 .UNSPECIFIED., .F., .F.,
 ( 4, 2, 4 ),
 ( 0.002365888236227967761, 0.003551327329835077609, 0.004736766423442186590 ),
 .UNSPECIFIED. ) ;
#10306=ORIENTED_EDGE ( 'NONE', *, *, #17283, .T. ) ;
#10315=DIRECTION ( 'NONE',  ( 1.000000000000000000, 0.000000000000000000, 0.000000000000000000 ) ) ;
#10321=ADVANCED_FACE ( 'NONE', ( #15985 ), #17644, .F. ) ;
#10342=CARTESIAN_POINT ( 'NONE',  ( 4.000000000000000000, 2.309401076758497151, -3.433295621305379353 ) ) ;
#10347=LINE ( 'NONE', #2922, #10993 ) ;
#10361=CIRCLE ( 'NONE', #4129, 5.384454397937118664 ) ;
#10372=CARTESIAN_POINT ( 'NONE',  ( -0.1410422978106123659, 4.700232962125094893, -3.687027686973624707 ) ) ;
#10387=AXIS2_PLACEMENT_3D ( 'NONE', #575, #8179, #672 ) ;
#10422=ORIENTED_EDGE ( 'NONE', *, *, #925, .T. ) ;
#10424=CARTESIAN_POINT ( 'NONE',  ( 4.000000000000000000, -2.471525695159793035, -3.686886880705770864 ) ) ;
#10449=CARTESIAN_POINT ( 'NONE',  ( -3.999999999998910649, -1.658469974638591804, -3.531532913075256186 ) ) ;
#10465=CARTESIAN_POINT ( 'NONE',  ( 3.540020015735602765, 2.810662092924382627, -3.602146406945867962 ) ) ;
#10466=CONICAL_SURFACE ( 'NONE', #5804, 2.059999999999998721, 0.9599310885968738161 ) ;
#10471=EDGE_CURVE ( 'NONE', #2762, #12007, #13049, .T. ) ;
#10475=B_SPLINE_CURVE_WITH_KNOTS ( 'NONE', 3,
 ( #16380, #2990, #18052, #9047, #8758, #15011 ),
 .UNSPECIFIED., .F., .F.,
 ( 4, 2, 4 ),
 ( 0.002365888236227977302, 0.003551327329835078910, 0.004736766423442180518 ),
 .UNSPECIFIED. ) ;
#10502=PRODUCT_DEFINITION_FORMATION_WITH_SPECIFIED_SOURCE ( 'ANY', '', #8424, .NOT_KNOWN. ) ;
#10539=EDGE_CURVE ( 'NONE', #13022, #12416, #6110, .T. ) ;
#10540=AXIS2_PLACEMENT_3D ( 'NONE', #7341, #19270, #11738 ) ;
#10576=VERTEX_POINT ( 'NONE', #13811 ) ;
#10612=DIRECTION ( 'NONE',  ( 0.000000000000000000, 0.000000000000000000, 1.000000000000000000 ) ) ;
#10624=ADVANCED_FACE ( 'NONE', ( #9318, #6306 ), #18128, .T. ) ;
#10640=CARTESIAN_POINT ( 'NONE',  ( -4.000000000000000000, -0.8232339106130515116, -3.430630286862743183 ) ) ;
#10673=CIRCLE ( 'NONE', #9111, 2.499999999999999556 ) ;
#10703=EDGE_LOOP ( 'NONE', ( #7373, #3911 ) ) ;
#10714=PLANE ( 'NONE',  #3276 ) ;
#10727=ORIENTED_EDGE ( 'NONE', *, *, #16035, .F. ) ;
#10729=SHAPE_REPRESENTATION_RELATIONSHIP ( 'NONE' , 'NONE' ,  #19222, #9020 ) ;
#10743=B_SPLINE_CURVE_WITH_KNOTS ( 'NONE', 3,
 ( #16961, #7780, #3572, #7874, #9532, #9143, #1721, #2110 ),
 .UNSPECIFIED., .F., .F.,
 ( 4, 2, 2, 4 ),
 ( 2.465131517390770070E-07, 0.001183067374689869946, 0.001774477805458935659, 0.002365888236228001588 ),
 .UNSPECIFIED. ) ;
#10809=CARTESIAN_POINT ( 'NONE',  ( -1.390230914382372118, -4.043987460488664532, -3.502507215260523665 ) ) ;
#10814=DIRECTION ( 'NONE',  ( -1.000000000000000000, 0.000000000000000000, 0.000000000000000000 ) ) ;
#10834=CARTESIAN_POINT ( 'NONE',  ( -4.000000000000000000, 0.3987449864459974846, -0.01220643443059782861 ) ) ;
#10839=CARTESIAN_POINT ( 'NONE',  ( -5.384454397937118664, 6.594054843588581554E-16, -4.484454397937119197 ) ) ;
#10850=VERTEX_POINT ( 'NONE', #1134 ) ;
#10865=CARTESIAN_POINT ( 'NONE',  ( -2.855764796983342624, 2.970025579236414082, -0.09382832055445475272 ) ) ;
#10886=FACE_OUTER_BOUND ( 'NONE', #4926, .T. ) ;
#10906=CARTESIAN_POINT ( 'NONE',  ( -3.510273485745307287, -2.827716139362669967, -3.610536846335890004 ) ) ;
#10933=ORIENTED_EDGE ( 'NONE', *, *, #2648, .T. ) ;
#10949=CARTESIAN_POINT ( 'NONE',  ( -1.393927851585477606, 4.043713361053528743, -3.526374918436835149 ) ) ;
#10952=ORIENTED_EDGE ( 'NONE', *, *, #7977, .F. ) ;
#10953=ORIENTED_EDGE ( 'NONE', *, *, #11156, .F. ) ;
#10957=CARTESIAN_POINT ( 'NONE',  ( -4.000000000000000000, 0.000000000000000000, 0.000000000000000000 ) ) ;
#10959=DIRECTION ( 'NONE',  ( -0.9396926207859138680, 0.000000000000000000, -0.3420201433256536139 ) ) ;
#10972=VERTEX_POINT ( 'NONE', #10125 ) ;
#10990=( GEOMETRIC_REPRESENTATION_CONTEXT ( 3 ) GLOBAL_UNCERTAINTY_ASSIGNED_CONTEXT ( ( #947 ) ) GLOBAL_UNIT_ASSIGNED_CONTEXT ( ( #8507, #14657, #7150 ) ) REPRESENTATION_CONTEXT ( 'NONE', 'WORKASPACE' ) );
#10993=VECTOR ( 'NONE', #18959, 1000.000000000000000 ) ;
#11003=DIRECTION ( 'NONE',  ( 0.000000000000000000, -0.000000000000000000, 1.000000000000000000 ) ) ;
#11016=EDGE_CURVE ( 'NONE', #6590, #2826, #6911, .T. ) ;
#11022=B_SPLINE_CURVE_WITH_KNOTS ( 'NONE', 3,
 ( #12512, #15447, #18479, #2059, #8017, #9583, #8310, #13976 ),
 .UNSPECIFIED., .F., .F.,
 ( 4, 2, 2, 4 ),
 ( 2.465131517071610173E-07, 0.001183067374689837636, 0.001774477805458902699, 0.002365888236227967761 ),
 .UNSPECIFIED. ) ;
#11044=DIRECTION ( 'NONE',  ( 0.000000000000000000, 0.000000000000000000, -1.000000000000000000 ) ) ;
#11072=EDGE_CURVE ( 'NONE', #9205, #11379, #18328, .T. ) ;
#11104=FACE_BOUND ( 'NONE', #10703, .T. ) ;
#11149=CARTESIAN_POINT ( 'NONE',  ( -4.000000000000000000, -2.309401076758515803, -0.4999999999999995559 ) ) ;
#11156=EDGE_CURVE ( 'NONE', #11820, #5897, #18041, .T. ) ;
#11176=CARTESIAN_POINT ( 'NONE',  ( -0.5636800770129166693, -4.293361309317430319, -3.531542292955206275 ) ) ;
#11208=CARTESIAN_POINT ( 'NONE',  ( 8.673617379884035472E-16, 4.618802153517012954, 0.000000000000000000 ) ) ;
#11219=VERTEX_POINT ( 'NONE', #16470 ) ;
#11233=DIRECTION ( 'NONE',  ( -1.000000000000000000, 0.000000000000000000, 0.000000000000000000 ) ) ;
#11239=ORIENTED_EDGE ( 'NONE', *, *, #6417, .F. ) ;
#11246=ORIENTED_EDGE ( 'NONE', *, *, #187, .F. ) ;
#11252=CARTESIAN_POINT ( 'NONE',  ( -5.560781378645573980, 0.000000000000000000, -4.000000000000000000 ) ) ;
#11272=EDGE_CURVE ( 'NONE', #8694, #13696, #18817, .T. ) ;
#11284=FACE_OUTER_BOUND ( 'NONE', #3090, .T. ) ;
#11322=ADVANCED_FACE ( 'NONE', ( #10886 ), #10466, .F. ) ;
#11339=DIRECTION ( 'NONE',  ( 1.000000000000000000, 0.000000000000000000, 0.000000000000000000 ) ) ;
#11379=VERTEX_POINT ( 'NONE', #11470 ) ;
#11381=CARTESIAN_POINT ( 'NONE',  ( 1.360585162435110629, -4.061296242128317857, -3.505054077164905024 ) ) ;
#11449=CARTESIAN_POINT ( 'NONE',  ( 4.211140560182196957, 2.431303136016536470, -3.745885042887433514 ) ) ;
#11470=CARTESIAN_POINT ( 'NONE',  ( -4.000000000000000000, 2.309401076758498483, -3.433295621305379353 ) ) ;
#11480=CONICAL_SURFACE ( 'NONE', #13970, 2.500000000000000888, 0.9599310885968785900 ) ;
#11485=VERTEX_POINT ( 'NONE', #18806 ) ;
#11487=VECTOR ( 'NONE', #8354, 1000.000000000000000 ) ;
#11501=AXIS2_PLACEMENT_3D ( 'NONE', #15946, #2748, #5780 ) ;
#11510=CARTESIAN_POINT ( 'NONE',  ( 0.000000000000000000, 0.000000000000000000, -4.974599999999998801 ) ) ;
#11536=ORIENTED_EDGE ( 'NONE', *, *, #9640, .F. ) ;
#11537=CARTESIAN_POINT ( 'NONE',  ( -4.198928548860774157, 0.8158838809860065044, -3.526471437616918170 ) ) ;
#11576=CARTESIAN_POINT ( 'NONE',  ( 2.725741868436127202, -3.045094352033990148, -3.220599429844051453 ) ) ;
#11599=DIRECTION ( 'NONE',  ( -1.000000000000000000, 0.000000000000000000, 0.000000000000000000 ) ) ;
#11626=CARTESIAN_POINT ( 'NONE',  ( -4.211140560182196957, 2.431303136016537803, -3.745885042887433514 ) ) ;
#11649=CARTESIAN_POINT ( 'NONE',  ( -4.141042297810615835, 2.227970268150415656, -3.687027686973619822 ) ) ;
#11696=CARTESIAN_POINT ( 'NONE',  ( 4.000000000000000000, -1.700175430507292473, -3.320327275037661785 ) ) ;
#11737=VERTEX_POINT ( 'NONE', #1239 ) ;
#11738=DIRECTION ( 'NONE',  ( 1.000000000000000000, 0.000000000000000000, 0.000000000000000000 ) ) ;
#11743=CARTESIAN_POINT ( 'NONE',  ( 1.567478505476134606E-15, 4.618802153517012066, -3.433295621305382905 ) ) ;
#11776=CARTESIAN_POINT ( 'NONE',  ( -3.333333333333335258, 2.694301256218251783, -3.300726591567079815 ) ) ;
#11787=EDGE_LOOP ( 'NONE', ( #16378, #15650, #9777, #1732, #14430 ) ) ;
#11790=DIRECTION ( 'NONE',  ( -0.000000000000000000, 0.000000000000000000, -1.000000000000000000 ) ) ;
#11808=CONICAL_SURFACE ( 'NONE', #18987, 2.500000000000000888, 0.9599310885968785900 ) ;
#11820=VERTEX_POINT ( 'NONE', #3874 ) ;
#11826=CARTESIAN_POINT ( 'NONE',  ( -1.149515148933662080E-15, -4.736529461166056443, -3.681130640444383317 ) ) ;
#11844=ORIENTED_EDGE ( 'NONE', *, *, #1712, .T. ) ;
#11849=CARTESIAN_POINT ( 'NONE',  ( -4.211140560182196957, 2.431303136016537803, -3.745885042887433514 ) ) ;
#11859=ORIENTED_EDGE ( 'NONE', *, *, #8651, .T. ) ;
#11867=DIRECTION ( 'NONE',  ( -1.000000000000000000, 0.000000000000000000, 0.000000000000000000 ) ) ;
#11870=CARTESIAN_POINT ( 'NONE',  ( -0.6666666666666651864, 4.233901974057260098, -3.300726591567081147 ) ) ;
#11880=ORIENTED_EDGE ( 'NONE', *, *, #925, .F. ) ;
#11914=CARTESIAN_POINT ( 'NONE',  ( -4.000000000000000000, 0.8576368993457507139, -3.433240632782198709 ) ) ;
#11916=EDGE_LOOP ( 'NONE', ( #12698, #18356, #2323 ) ) ;
#11937=DIRECTION ( 'NONE',  ( -0.000000000000000000, -0.000000000000000000, 1.000000000000000000 ) ) ;
#11997=CARTESIAN_POINT ( 'NONE',  ( -4.211140560182196957, -2.431303136016552013, -3.745885042887436178 ) ) ;
#12003=( NAMED_UNIT ( * ) PLANE_ANGLE_UNIT ( ) SI_UNIT ( $, .RADIAN. ) );
#12007=VERTEX_POINT ( 'NONE', #17145 ) ;
#12028=CARTESIAN_POINT ( 'NONE',  ( 3.472371940585993855, 2.614027278893175321, -3.320322319201766792 ) ) ;
#12030=CARTESIAN_POINT ( 'NONE',  ( 2.000000000000008882, 3.464101615137749945, 0.000000000000000000 ) ) ;
#12035=ORIENTED_EDGE ( 'NONE', *, *, #161, .F. ) ;
#12048=EDGE_LOOP ( 'NONE', ( #5327, #16142, #556, #8237 ) ) ;
#12064=B_SPLINE_CURVE_WITH_KNOTS ( 'NONE', 3,
 ( #758, #6522, #566, #2301, #3867, #8267, #14215, #18435 ),
 .UNSPECIFIED., .F., .F.,
 ( 4, 2, 2, 4 ),
 ( 0.000000000000000000, 0.002450665683189819262, 0.003675998524784728893, 0.004901331366379639391 ),
 .UNSPECIFIED. ) ;
#12073=CARTESIAN_POINT ( 'NONE',  ( 0.000000000000000000, 0.000000000000000000, -4.484454397937119197 ) ) ;
#12106=TOROIDAL_SURFACE ( 'NONE', #12413, 5.384454397937118664, 0.5155456020628804703 ) ;
#12119=EDGE_CURVE ( 'NONE', #1583, #7197, #3000, .T. ) ;
#12136=VERTEX_POINT ( 'NONE', #6571 ) ;
#12139=EDGE_CURVE ( 'NONE', #10188, #11820, #18610, .T. ) ;
#12154=CARTESIAN_POINT ( 'NONE',  ( -2.100000000000000089, 2.571758278209441957E-16, -0.2800830152838844622 ) ) ;
#12161=DIRECTION ( 'NONE',  ( 0.000000000000000000, 0.000000000000000000, -1.000000000000000000 ) ) ;
#12163=CARTESIAN_POINT ( 'NONE',  ( 1.828356344711641102, 3.563200125723180900, -5.433716356636336675E-16 ) ) ;
#12183=CARTESIAN_POINT ( 'NONE',  ( -3.453038570459499024, -2.625189405340453419, -3.535263753545272891 ) ) ;
#12186=ORIENTED_EDGE ( 'NONE', *, *, #16770, .T. ) ;
#12212=FACE_OUTER_BOUND ( 'NONE', #8314, .T. ) ;
#12242=AXIS2_PLACEMENT_3D ( 'NONE', #14852, #16709, #4805 ) ;
#12259=EDGE_CURVE ( 'NONE', #10850, #12903, #16567, .T. ) ;
#12281=DIRECTION ( 'NONE',  ( -1.000000000000000000, 0.000000000000000000, 0.000000000000000000 ) ) ;
#12283=CARTESIAN_POINT ( 'NONE',  ( -2.756197834950067094, -3.027510591568735254, -3.223146290109809797 ) ) ;
#12293=DIRECTION ( 'NONE',  ( -0.000000000000000000, -0.000000000000000000, 1.000000000000000000 ) ) ;
#12302=CARTESIAN_POINT ( 'NONE',  ( 4.024499207728848837, 2.323545700935681246, -3.572172305156870564 ) ) ;
#12305=EDGE_LOOP ( 'NONE', ( #2079, #7394 ) ) ;
#12321=EDGE_LOOP ( 'NONE', ( #18271, #12782, #9681, #10953 ) ) ;
#12322=CARTESIAN_POINT ( 'NONE',  ( -4.211140560182196957, -2.431303136016552013, -3.745885042887436178 ) ) ;
#12323=CARTESIAN_POINT ( 'NONE',  ( -2.688821387764050996E-14, -4.618802153517012954, -0.4999999999999995559 ) ) ;
#12324=CARTESIAN_POINT ( 'NONE',  ( 4.000000000000000000, 0.7924765000094659007, -0.05906175389889852662 ) ) ;
#12334=CARTESIAN_POINT ( 'NONE',  ( -4.000000000000000000, 2.309401076758498483, -0.4999999999999927280 ) ) ;
#12368=DIRECTION ( 'NONE',  ( 0.8191520442889875797, 0.000000000000000000, 0.5735764363510522656 ) ) ;
#12378=CARTESIAN_POINT ( 'NONE',  ( -2.500000000000000444, 3.061616997868383634E-16, -5.000000000000000888 ) ) ;
#12404=CARTESIAN_POINT ( 'NONE',  ( -2.682243648011671588, -3.070208061305317759, -0.04852650426602272971 ) ) ;
#12412=ORIENTED_EDGE ( 'NONE', *, *, #17331, .T. ) ;
#12413=AXIS2_PLACEMENT_3D ( 'NONE', #8221, #5101, #1965 ) ;
#12416=VERTEX_POINT ( 'NONE', #2741 ) ;
#12419=CARTESIAN_POINT ( 'NONE',  ( 3.999999999999999112, 1.941961291383486277, -0.3515519931180248192 ) ) ;
#12422=AXIS2_PLACEMENT_3D ( 'NONE', #10253, #15027, #17778 ) ;
#12448=EDGE_CURVE ( 'NONE', #11379, #15250, #13541, .T. ) ;
#12458=ORIENTED_EDGE ( 'NONE', *, *, #9491, .T. ) ;
#12462=ORIENTED_EDGE ( 'NONE', *, *, #187, .T. ) ;
#12464=B_SPLINE_CURVE_WITH_KNOTS ( 'NONE', 3,
 ( #19159, #16130, #17692, #1285, #19065 ),
 .UNSPECIFIED., .F., .F.,
 ( 4, 1, 4 ),
 ( 5.640274452250024914E-20, 0.002309401076758505356, 0.004618802153517010713 ),
 .UNSPECIFIED. ) ;
#12503=EDGE_LOOP ( 'NONE', ( #14450, #15541, #12458, #9379, #10933 ) ) ;
#12509=ORIENTED_EDGE ( 'NONE', *, *, #3784, .F. ) ;
#12512=CARTESIAN_POINT ( 'NONE',  ( 4.000000000000000000, -2.309401076758516691, -0.4999999999999995559 ) ) ;
#12585=ORIENTED_EDGE ( 'NONE', *, *, #7168, .T. ) ;
#12586=EDGE_LOOP ( 'NONE', ( #16604, #8495, #16922, #18557 ) ) ;
#12611=CARTESIAN_POINT ( 'NONE',  ( 4.154306624730763176, -2.398490048084970461, -3.721999068284303824 ) ) ;
#12673=PRODUCT_CONTEXT ( 'NONE', #94, 'mechanical' ) ;
#12697=EDGE_CURVE ( 'NONE', #4279, #9797, #18690, .T. ) ;
#12698=ORIENTED_EDGE ( 'NONE', *, *, #14007, .T. ) ;
#12706=CARTESIAN_POINT ( 'NONE',  ( 0.000000000000000000, 0.000000000000000000, 3.469446951953614189E-15 ) ) ;
#12708=B_SPLINE_CURVE_WITH_KNOTS ( 'NONE', 3,
 ( #13280, #19157, #8884, #5592, #2835, #19062 ),
 .UNSPECIFIED., .F., .F.,
 ( 4, 2, 4 ),
 ( 0.002452478801916361129, 0.003676905084148001344, 0.004901331366379641126 ),
 .UNSPECIFIED. ) ;
#12758=DIRECTION ( 'NONE',  ( -0.000000000000000000, -0.000000000000000000, 1.000000000000000000 ) ) ;
#12782=ORIENTED_EDGE ( 'NONE', *, *, #15458, .T. ) ;
#12825=DIRECTION ( 'NONE',  ( -0.000000000000000000, -0.000000000000000000, 1.000000000000000000 ) ) ;
#12827=CARTESIAN_POINT ( 'NONE',  ( -3.436319922987618902, 2.634841920961291439, -3.531542292955721862 ) ) ;
#12849=CARTESIAN_POINT ( 'NONE',  ( -0.02448733951239248641, -4.877042772274742255, -3.751161874094027571 ) ) ;
#12862=CARTESIAN_POINT ( 'NONE',  ( -4.211140560182196957, 2.431303136016537803, -3.745885042887433514 ) ) ;
#12882=AXIS2_PLACEMENT_3D ( 'NONE', #10839, #9472, #15243 ) ;
#12903=VERTEX_POINT ( 'NONE', #3747 ) ;
#12918=ORIENTED_EDGE ( 'NONE', *, *, #8174, .F. ) ;
#12921=CARTESIAN_POINT ( 'NONE',  ( -0.6640947660597427138, 4.471078309994878985, -3.602146406945963442 ) ) ;
#12939=ADVANCED_FACE ( 'NONE', ( #1729 ), #3059, .T. ) ;
#12942=CARTESIAN_POINT ( 'NONE',  ( 1.243802165048773611, -3.900692638707475624, -3.223146290109810241 ) ) ;
#12953=CARTESIAN_POINT ( 'NONE',  ( 4.211140560182196957, 2.431303136016536470, -3.745885042887433514 ) ) ;
#12984=ADVANCED_FACE ( 'NONE', ( #378 ), #15415, .F. ) ;
#13022=VERTEX_POINT ( 'NONE', #12378 ) ;
#13049=LINE ( 'NONE', #7376, #8595 ) ;
#13053=CARTESIAN_POINT ( 'NONE',  ( 0.000000000000000000, 0.000000000000000000, 0.000000000000000000 ) ) ;
#13084=SURFACE_STYLE_FILL_AREA ( #19149 ) ;
#13135=DIRECTION ( 'NONE',  ( 0.9396926207859138680, 1.150791560227856926E-16, -0.3420201433256536139 ) ) ;
#13158=FACE_OUTER_BOUND ( 'NONE', #15934, .T. ) ;
#13184=MECHANICAL_DESIGN_GEOMETRIC_PRESENTATION_REPRESENTATION('',(#5710),#10990);
#13200=ORIENTED_EDGE ( 'NONE', *, *, #8651, .F. ) ;
#13202=CARTESIAN_POINT ( 'NONE',  ( 2.836893136758676270, 3.208949435745843903, -3.505054077164911241 ) ) ;
#13234=DIRECTION ( 'NONE',  ( 0.000000000000000000, -0.000000000000000000, 1.000000000000000000 ) ) ;
#13249=CARTESIAN_POINT ( 'NONE',  ( 2.059999999999998721, 0.000000000000000000, -0.3080913168122742518 ) ) ;
#13279=CARTESIAN_POINT ( 'NONE',  ( -4.000000000000000000, -0.8382240730041925492, -3.220610619767135141 ) ) ;
#13280=CARTESIAN_POINT ( 'NONE',  ( 4.197393957002303999, 7.772902908466098641E-14, -3.503767560748929810 ) ) ;
#13330=CARTESIAN_POINT ( 'NONE',  ( -4.000000000000000000, 2.309401076758498483, -5.000000000000000000 ) ) ;
#13344=CIRCLE ( 'NONE', #5867, 5.560781378645573980 ) ;
#13386=CARTESIAN_POINT ( 'NONE',  ( -3.264624719419710521E-13, -4.796980096169328966, -3.721999068284310486 ) ) ;
#13393=DIRECTION ( 'NONE',  ( 1.000000000000000000, 0.000000000000000000, 0.000000000000000000 ) ) ;
#13403=FACE_OUTER_BOUND ( 'NONE', #3435, .T. ) ;
#13405=EDGE_CURVE ( 'NONE', #14097, #11379, #15670, .T. ) ;
#13452=CARTESIAN_POINT ( 'NONE',  ( 4.000000000001088907, 1.658577278524410170, -3.531553309554541720 ) ) ;
#13454=EDGE_CURVE ( 'NONE', #11219, #12136, #8321, .T. ) ;
#13473=VERTEX_POINT ( 'NONE', #2262 ) ;
#13484=DIRECTION ( 'NONE',  ( 0.000000000000000000, 0.000000000000000000, -1.000000000000000000 ) ) ;
#13488=EDGE_LOOP ( 'NONE', ( #12462, #18140, #19063, #8525 ) ) ;
#13491=CARTESIAN_POINT ( 'NONE',  ( 4.235886605889389145, 2.417314728048528760, -3.751161874094018245 ) ) ;
#13494=CARTESIAN_POINT ( 'NONE',  ( 2.344047193898588954, 3.265465875126468021, -5.031375706690542042E-16 ) ) ;
#13538=DIRECTION ( 'NONE',  ( -1.000000000000000000, 0.000000000000000000, 0.000000000000000000 ) ) ;
#13541=B_SPLINE_CURVE_WITH_KNOTS ( 'NONE', 3,
 ( #14365, #1189, #8600, #14551, #4114 ),
 .UNSPECIFIED., .F., .F.,
 ( 4, 1, 4 ),
 ( 0.000000000000000000, 0.002309401076758505790, 0.004618802153517011580 ),
 .UNSPECIFIED. ) ;
#13542=CARTESIAN_POINT ( 'NONE',  ( 4.000000000000000000, -0.8732470631449981147, -3.223155494240760088 ) ) ;
#13544=CARTESIAN_POINT ( 'NONE',  ( -4.000000000000000000, 2.309401076758498483, -5.000000000000000000 ) ) ;
#13569=CARTESIAN_POINT ( 'NONE',  ( -4.000000000000000000, 0.9868501483902560878, -0.09357334158579519445 ) ) ;
#13570=CARTESIAN_POINT ( 'NONE',  ( -6.473970235329672780E-16, -4.862606272033106691, -3.745885042887442395 ) ) ;
#13618=CARTESIAN_POINT ( 'NONE',  ( 1.654252653721905331, 3.663718938583014229, -0.01223254789873410957 ) ) ;
#13643=CARTESIAN_POINT ( 'NONE',  ( -0.6810597143197697489, -4.461075778259609770, -3.598441714920717516 ) ) ;
#13646=VECTOR ( 'NONE', #1960, 1000.000000000000114 ) ;
#13681=CARTESIAN_POINT ( 'NONE',  ( 3.999999999999999112, -0.7890432684750902093, -0.04868663549882291247 ) ) ;
#13686=AXIS2_PLACEMENT_3D ( 'NONE', #14956, #3224, #1580 ) ;
#13692=EDGE_CURVE ( 'NONE', #2826, #2762, #8910, .T. ) ;
#13696=VERTEX_POINT ( 'NONE', #2544 ) ;
#13727=PRODUCT_DEFINITION_CONTEXT ( 'detailed design', #6962, 'design' ) ;
#13748=DIRECTION ( 'NONE',  ( 0.000000000000000000, 0.000000000000000000, -1.000000000000000000 ) ) ;
#13809=CIRCLE ( 'NONE', #3522, 4.000000000000000000 ) ;
#13811=CARTESIAN_POINT ( 'NONE',  ( 5.384454397937118664, 0.000000000000000000, -5.000000000000000000 ) ) ;
#13851=CARTESIAN_POINT ( 'NONE',  ( 4.211140560182196957, -2.431303136016555122, -3.745885042887436622 ) ) ;
#13855=CARTESIAN_POINT ( 'NONE',  ( -2.500000000000000444, 3.061616997868383634E-16, -25.03750572909317285 ) ) ;
#13870=DIRECTION ( 'NONE',  ( -1.000000000000000000, 0.000000000000000000, 0.000000000000000000 ) ) ;
#13872=UNCERTAINTY_MEASURE_WITH_UNIT (LENGTH_MEASURE( 1.000000000000000082E-05 ), #7702, 'distance_accuracy_value', 'NONE');
#13948=AXIS2_PLACEMENT_3D ( 'NONE', #965, #18743, #1147 ) ;
#13970=AXIS2_PLACEMENT_3D ( 'NONE', #11510, #15813, #11599 ) ;
#13976=CARTESIAN_POINT ( 'NONE',  ( 2.000000000000005329, -3.464101615137751722, 0.000000000000000000 ) ) ;
#14007=EDGE_CURVE ( 'NONE', #11485, #13696, #2132, .T. ) ;
#14051=EDGE_CURVE ( 'NONE', #6590, #9205, #7050, .T. ) ;
#14055=ORIENTED_EDGE ( 'NONE', *, *, #3784, .T. ) ;
#14077=ORIENTED_EDGE ( 'NONE', *, *, #2183, .T. ) ;
#14079=CARTESIAN_POINT ( 'NONE',  ( 0.000000000000000000, 0.000000000000000000, -4.694516984716113228 ) ) ;
#14089=ORIENTED_EDGE ( 'NONE', *, *, #770, .T. ) ;
#14097=VERTEX_POINT ( 'NONE', #12862 ) ;
#14143=DIRECTION ( 'NONE',  ( -1.000000000000000000, 0.000000000000000000, 0.000000000000000000 ) ) ;
#14215=CARTESIAN_POINT ( 'NONE',  ( 0.3461262719736147297, -4.658553426539303821, -3.671615880910379381 ) ) ;
#14218=( GEOMETRIC_REPRESENTATION_CONTEXT ( 3 ) GLOBAL_UNCERTAINTY_ASSIGNED_CONTEXT ( ( #13872 ) ) GLOBAL_UNIT_ASSIGNED_CONTEXT ( ( #7702, #12003, #16692 ) ) REPRESENTATION_CONTEXT ( 'NONE', 'WORKASPACE' ) );
#14262=CARTESIAN_POINT ( 'NONE',  ( -1.747541505913277282, 3.837784562140256650, -3.503702292528906526 ) ) ;
#14308=CARTESIAN_POINT ( 'NONE',  ( 4.236525694536557474, -2.416953475386482530, -3.751298745799839462 ) ) ;
#14319=CARTESIAN_POINT ( 'NONE',  ( -3.974357786152442180E-13, 4.796734841935204052, -3.721909803043259579 ) ) ;
#14320=PLANE ( 'NONE',  #5724 ) ;
#14365=CARTESIAN_POINT ( 'NONE',  ( -4.000000000000000000, 2.309401076758498483, -3.433295621305379353 ) ) ;
#14372=FACE_OUTER_BOUND ( 'NONE', #12048, .T. ) ;
#14419=CIRCLE ( 'NONE', #2270, 2.100000000000000089 ) ;
#14430=ORIENTED_EDGE ( 'NONE', *, *, #9640, .T. ) ;
#14450=ORIENTED_EDGE ( 'NONE', *, *, #2183, .F. ) ;
#14461=CARTESIAN_POINT ( 'NONE',  ( -0.6666666666666666297, -4.233901974057276973, -3.300726591567087365 ) ) ;
#14464=VERTEX_POINT ( 'NONE', #16617 ) ;
#14519=CARTESIAN_POINT ( 'NONE',  ( 0.000000000000000000, 0.000000000000000000, 0.000000000000000000 ) ) ;
#14551=CARTESIAN_POINT ( 'NONE',  ( -4.000000000000000888, -1.539600717839011201, -3.300726591567081591 ) ) ;
#14556=CARTESIAN_POINT ( 'NONE',  ( -6.259644161404860030E-16, -4.618802153517027165, -3.433295621305388234 ) ) ;
#14569=VECTOR ( 'NONE', #10612, 1000.000000000000000 ) ;
#14596=ORIENTED_EDGE ( 'NONE', *, *, #1136, .F. ) ;
#14620=FACE_OUTER_BOUND ( 'NONE', #18679, .T. ) ;
#14657=( NAMED_UNIT ( * ) PLANE_ANGLE_UNIT ( ) SI_UNIT ( $, .RADIAN. ) );
#14728=FACE_OUTER_BOUND ( 'NONE', #771, .T. ) ;
#14744=CIRCLE ( 'NONE', #12882, 0.5155456020628804703 ) ;
#14778=PRODUCT_DEFINITION ( 'UNKNOWN', '', #10502, #13727 ) ;
#14852=CARTESIAN_POINT ( 'NONE',  ( 1.567478505476134606E-15, 4.618802153517012066, -5.000000000000000000 ) ) ;
#14853=STYLED_ITEM ( 'NONE', ( #8690 ), #9020 ) ;
#14854=CARTESIAN_POINT ( 'NONE',  ( -3.333333333333332149, -2.694301256218264218, -3.300726591567082036 ) ) ;
#14876=( BOUNDED_SURFACE ( )  B_SPLINE_SURFACE ( 3, 2, ( 
 ( #14921, #10424, #19228 ),
 ( #11696, #17665, #4565 ),
 ( #13542, #1548, #10241 ),
 ( #2811, #6039, #16205 ),
 ( #1355, #13452, #17767 ),
 ( #183, #7298, #1442 ) ),
 .UNSPECIFIED., .F., .F., .F. ) 
 B_SPLINE_SURFACE_WITH_KNOTS ( ( 4, 2, 4 ),
 ( 3, 3 ),
 ( 0.02027065861071770947, 0.02273072267836921331, 0.02519078674602071716 ),
 ( 0.000000000000000000, 1.000000000000000000 ),
 .UNSPECIFIED. ) 
 GEOMETRIC_REPRESENTATION_ITEM ( )  RATIONAL_B_SPLINE_SURFACE ( (
 ( 1.000000000000000000, 0.8047781708337304885, 1.000000000000000000),
 ( 1.000000000000000000, 0.8123765190705307671, 1.000000000000000000),
 ( 1.000000000000000000, 0.8190656277163975707, 1.000000000000000000),
 ( 1.000000000000000000, 0.8192366903512159348, 1.000000000000000000),
 ( 1.000000000000000000, 0.8126138454302893610, 1.000000000000000000),
 ( 1.000000000000000000, 0.8047712246031417660, 1.000000000000000000) ) ) 
 REPRESENTATION_ITEM ( '' )  SURFACE ( )  );
#14914=CIRCLE ( 'NONE', #7110, 2.100000000000000089 ) ;
#14921=CARTESIAN_POINT ( 'NONE',  ( 4.000000000000000000, -2.511475576507276042, -3.469253905236643565 ) ) ;
#14923=VECTOR ( 'NONE', #8838, 1000.000000000000000 ) ;
#14946=CARTESIAN_POINT ( 'NONE',  ( -4.197312064133472020, -0.8182229787990021874, -3.502518405183886685 ) ) ;
#14956=CARTESIAN_POINT ( 'NONE',  ( 0.000000000000000000, 0.000000000000000000, -5.000000000000000000 ) ) ;
#14988=CARTESIAN_POINT ( 'NONE',  ( 0.000000000000000000, 0.000000000000000000, -4.000000000000000000 ) ) ;
#14994=LINE ( 'NONE', #5727, #6509 ) ;
#15011=CARTESIAN_POINT ( 'NONE',  ( 1.734723475976807094E-15, 4.618802153517012954, -0.4999999999999995559 ) ) ;
#15027=DIRECTION ( 'NONE',  ( 0.000000000000000000, 0.000000000000000000, -1.000000000000000000 ) ) ;
#15038=CARTESIAN_POINT ( 'NONE',  ( 4.154306624730864428, 2.398490048084778170, -3.721999068284300272 ) ) ;
#15041=VERTEX_POINT ( 'NONE', #18257 ) ;
#15051=CARTESIAN_POINT ( 'NONE',  ( 3.999999999999999112, -0.3979232138631231819, -5.929230630780099908E-17 ) ) ;
#15055=CARTESIAN_POINT ( 'NONE',  ( 0.5636800770130377947, 4.293361309317166530, -3.531542292954102713 ) ) ;
#15092=CARTESIAN_POINT ( 'NONE',  ( 0.6448876103708359731, 4.246476118072354922, -0.2256878752776725616 ) ) ;
#15101=DIRECTION ( 'NONE',  ( -0.000000000000000000, -0.000000000000000000, 1.000000000000000000 ) ) ;
#15113=CARTESIAN_POINT ( 'NONE',  ( -2.836893136758495970, -3.208949435745868328, -3.505054077164885484 ) ) ;
#15123=ADVANCED_FACE ( 'NONE', ( #11104, #386 ), #18352, .F. ) ;
#15136=CARTESIAN_POINT ( 'NONE',  ( -4.204114297095464359, 1.660363174096617156, -3.602136431857887011 ) ) ;
#15140=AXIS2_PLACEMENT_3D ( 'NONE', #19231, #1160, #19131 ) ;
#15155=CARTESIAN_POINT ( 'NONE',  ( 4.000000000000000000, 0.1981133338132474442, 2.382280164152719704E-17 ) ) ;
#15206=CARTESIAN_POINT ( 'NONE',  ( -6.473970235329672780E-16, -4.862606272033106691, -3.745885042887442395 ) ) ;
#15221=CARTESIAN_POINT ( 'NONE',  ( -2.000000000000007550, -3.464101615137749945, 0.000000000000000000 ) ) ;
#15243=DIRECTION ( 'NONE',  ( -1.000000000000000000, 1.224646799147352714E-16, 0.000000000000000000 ) ) ;
#15250=VERTEX_POINT ( 'NONE', #15991 ) ;
#15254=EDGE_LOOP ( 'NONE', ( #10727, #14089, #6690 ) ) ;
#15258=ORIENTED_EDGE ( 'NONE', *, *, #16770, .F. ) ;
#15315=EDGE_LOOP ( 'NONE', ( #9663, #5104, #18306, #9386 ) ) ;
#15344=CARTESIAN_POINT ( 'NONE',  ( -2.500000000000000888, 0.000000000000000000, -4.974599999999998801 ) ) ;
#15371=DIRECTION ( 'NONE',  ( 0.000000000000000000, 0.000000000000000000, 1.000000000000000000 ) ) ;
#15382=CLOSED_SHELL ( 'NONE', ( #663, #18454, #11322, #18549, #4355, #9518, #6488, #7662, #7721, #4718, #8156, #8371, #10037, #15123, #10624, #16203, #2112, #17602, #19201, #18811, #4695, #4222, #12939, #12984, #16754, #5669, #6155, #2317, #3364, #5220, #4608, #10321 ) ) ;
#15390=DIRECTION ( 'NONE',  ( -1.000000000000000000, 0.000000000000000000, 0.000000000000000000 ) ) ;
#15415=( BOUNDED_SURFACE ( )  B_SPLINE_SURFACE ( 3, 2, ( 
 ( #4966, #18804, #15675 ),
 ( #9150, #12183, #3843 ),
 ( #12283, #2284, #15113 ),
 ( #7686, #15771, #10809 ),
 ( #284, #11176, #13643 ),
 ( #17142, #2380, #8248 ) ),
 .UNSPECIFIED., .F., .F., .F. ) 
 B_SPLINE_SURFACE_WITH_KNOTS ( ( 4, 2, 4 ),
 ( 3, 3 ),
 ( 0.02032853247518126918, 0.02278863295364821906, 0.02524873343211516893 ),
 ( 0.000000000000000000, 1.000000000000000000 ),
 .UNSPECIFIED. ) 
 GEOMETRIC_REPRESENTATION_ITEM ( )  RATIONAL_B_SPLINE_SURFACE ( (
 ( 1.000000000000000000, 0.8047781615896838492, 1.000000000000000000),
 ( 1.000000000000000000, 0.8123767586288186404, 1.000000000000000000),
 ( 1.000000000000000000, 0.8190662415565814758, 1.000000000000000000),
 ( 1.000000000000000000, 0.8192361015667604107, 1.000000000000000000),
 ( 1.000000000000000000, 0.8126135807104967190, 1.000000000000000000),
 ( 1.000000000000000000, 0.8047712338318580017, 1.000000000000000000) ) ) 
 REPRESENTATION_ITEM ( '' )  SURFACE ( )  );
#15447=CARTESIAN_POINT ( 'NONE',  ( 3.680118525130245732, -2.494084732383344605, -0.3507732604232533524 ) ) ;
#15458=EDGE_CURVE ( 'NONE', #10188, #1970, #3173, .T. ) ;
#15527=ORIENTED_EDGE ( 'NONE', *, *, #16544, .F. ) ;
#15541=ORIENTED_EDGE ( 'NONE', *, *, #3943, .T. ) ;
#15571=CARTESIAN_POINT ( 'NONE',  ( 4.000000000000000000, 2.309401076758497151, -5.000000000000000000 ) ) ;
#15604=EDGE_CURVE ( 'NONE', #15250, #10850, #5213, .T. ) ;
#15614=CARTESIAN_POINT ( 'NONE',  ( 0.000000000000000000, 0.000000000000000000, 0.000000000000000000 ) ) ;
#15645=CARTESIAN_POINT ( 'NONE',  ( -6.259644161404860030E-16, -4.618802153517027165, -3.433295621305388234 ) ) ;
#15650=ORIENTED_EDGE ( 'NONE', *, *, #12448, .T. ) ;
#15670=B_SPLINE_CURVE_WITH_KNOTS ( 'NONE', 3,
 ( #11849, #4825, #3339, #16348, #1504, #4523 ),
 .UNSPECIFIED., .F., .F.,
 ( 4, 2, 4 ),
 ( -3.640115492410698714E-06, 0.0002066546034003381217, 0.0004169493222930869755 ),
 .UNSPECIFIED. ) ;
#15671=ORIENTED_EDGE ( 'NONE', *, *, #7478, .F. ) ;
#15675=CARTESIAN_POINT ( 'NONE',  ( -4.235886605889389145, -2.417314728048544303, -3.751161874094020909 ) ) ;
#15771=CARTESIAN_POINT ( 'NONE',  ( -1.287237434361707233, -3.875615274277397937, -3.430618716626816500 ) ) ;
#15783=CARTESIAN_POINT ( 'NONE',  ( 2.807080416178989513, -3.225969019225150003, -3.502507215260505014 ) ) ;
#15813=DIRECTION ( 'NONE',  ( 0.000000000000000000, 0.000000000000000000, -1.000000000000000000 ) ) ;
#15893=DIRECTION ( 'NONE',  ( 0.8660254037844374864, -0.5000000000000018874, 0.000000000000000000 ) ) ;
#15934=EDGE_LOOP ( 'NONE', ( #6558, #17328, #6734, #6443, #18582 ) ) ;
#15942=CARTESIAN_POINT ( 'NONE',  ( 4.197393957002303999, 7.772902908466098641E-14, -3.503767560748929810 ) ) ;
#15946=CARTESIAN_POINT ( 'NONE',  ( 0.000000000000000000, 0.000000000000000000, -4.000000000000000000 ) ) ;
#15956=VERTEX_POINT ( 'NONE', #15221 ) ;
#15985=FACE_OUTER_BOUND ( 'NONE', #5693, .T. ) ;
#15991=CARTESIAN_POINT ( 'NONE',  ( -4.000000000000000000, -2.309401076758512694, -3.433295621305382461 ) ) ;
#16009=AXIS2_PLACEMENT_3D ( 'NONE', #9250, #11003, #10814 ) ;
#16030=DIRECTION ( 'NONE',  ( -0.000000000000000000, -0.000000000000000000, 1.000000000000000000 ) ) ;
#16035=EDGE_CURVE ( 'NONE', #14464, #13696, #2417, .T. ) ;
#16070=CARTESIAN_POINT ( 'NONE',  ( -0.1404048886732797152, -4.699864953788083888, -3.686887068327043160 ) ) ;
#16076=AXIS2_PLACEMENT_3D ( 'NONE', #7232, #4403, #8598 ) ;
#16099=DIRECTION ( 'NONE',  ( 0.000000000000000000, 0.000000000000000000, 1.000000000000000000 ) ) ;
#16120=SURFACE_STYLE_USAGE ( .BOTH. , #4196 ) ;
#16123=EDGE_CURVE ( 'NONE', #10576, #12007, #8344, .T. ) ;
#16130=CARTESIAN_POINT ( 'NONE',  ( 0.6666666666666658525, -4.233901974057276085, -3.300726591567086476 ) ) ;
#16142=ORIENTED_EDGE ( 'NONE', *, *, #5326, .T. ) ;
#16172=AXIS2_PLACEMENT_3D ( 'NONE', #1060, #18940, #14143 ) ;
#16203=ADVANCED_FACE ( 'NONE', ( #8656 ), #19279, .T. ) ;
#16205=CARTESIAN_POINT ( 'NONE',  ( 4.197310751797292738, 0.8178363989516252985, -3.502498386812444409 ) ) ;
#16229=CARTESIAN_POINT ( 'NONE',  ( -4.211405944401398038, -2.460460786169389902, -3.751298493805494072 ) ) ;
#16250=ORIENTED_EDGE ( 'NONE', *, *, #16523, .T. ) ;
#16269=CARTESIAN_POINT ( 'NONE',  ( -4.154094228333820915, -2.398367420967594921, -3.721909803043257803 ) ) ;
#16285=EDGE_LOOP ( 'NONE', ( #11536, #11859, #15671 ) ) ;
#16287=CARTESIAN_POINT ( 'NONE',  ( -6.259644161404860030E-16, -4.618802153517027165, -5.000000000000000000 ) ) ;
#16321=CARTESIAN_POINT ( 'NONE',  ( -4.000000000000000000, 0.8730739991738342143, -3.223134629628428893 ) ) ;
#16348=CARTESIAN_POINT ( 'NONE',  ( -4.024497503033714452, 2.323544716729487813, -3.572167766733750582 ) ) ;
#16378=ORIENTED_EDGE ( 'NONE', *, *, #5320, .F. ) ;
#16380=CARTESIAN_POINT ( 'NONE',  ( -2.000000000000006661, 3.464101615137750834, 0.000000000000000000 ) ) ;
#16423=EDGE_CURVE ( 'NONE', #4279, #16577, #7674, .T. ) ;
#16425=FACE_OUTER_BOUND ( 'NONE', #19098, .T. ) ;
#16430=EDGE_LOOP ( 'NONE', ( #19218, #86, #8858 ) ) ;
#16432=CARTESIAN_POINT ( 'NONE',  ( -0.1756481739660520902, 4.720212674038980261, -3.469390959564065291 ) ) ;
#16448=CIRCLE ( 'NONE', #6796, 2.500000000000000888 ) ;
#16457=B_SPLINE_CURVE_WITH_KNOTS ( 'NONE', 3,
 ( #4890, #598, #10834, #1666, #13569, #3312, #3414, #3505 ),
 .UNSPECIFIED., .F., .F.,
 ( 4, 2, 2, 4 ),
 ( 0.005725059856848641743, 0.006314084072593626612, 0.006903108288338611481, 0.008081156719828581220 ),
 .UNSPECIFIED. ) ;
#16470=CARTESIAN_POINT ( 'NONE',  ( -4.197393957002303999, -7.773935952363655451E-14, -3.503767560748929810 ) ) ;
#16476=AXIS2_PLACEMENT_3D ( 'NONE', #2808, #13538, #16099 ) ;
#16513=CARTESIAN_POINT ( 'NONE',  ( -4.000000000000000000, -2.512220745329312610, -3.469390707569719901 ) ) ;
#16523=EDGE_CURVE ( 'NONE', #11485, #8694, #10475, .T. ) ;
#16542=LINE ( 'NONE', #1686, #5426 ) ;
#16544=EDGE_CURVE ( 'NONE', #5897, #10972, #1348, .T. ) ;
#16567=B_SPLINE_CURVE_WITH_KNOTS ( 'NONE', 3,
 ( #11149, #17118, #8128, #5110, #9391, #10957 ),
 .UNSPECIFIED., .F., .F.,
 ( 4, 2, 4 ),
 ( 0.003358874760055550156, 0.004541967308452096383, 0.005725059856848641743 ),
 .UNSPECIFIED. ) ;
#16577=VERTEX_POINT ( 'NONE', #3569 ) ;
#16604=ORIENTED_EDGE ( 'NONE', *, *, #5307, .F. ) ;
#16607=CARTESIAN_POINT ( 'NONE',  ( -4.203934362469166963, -1.640673743454851286, -3.598432614606932756 ) ) ;
#16617=CARTESIAN_POINT ( 'NONE',  ( 4.000000000000000000, 0.000000000000000000, 0.000000000000000000 ) ) ;
#16626=CIRCLE ( 'NONE', #6323, 2.100000000000000089 ) ;
#16665=CARTESIAN_POINT ( 'NONE',  ( 0.000000000000000000, 0.000000000000000000, 0.000000000000000000 ) ) ;
#16692=( NAMED_UNIT ( * ) SI_UNIT ( $, .STERADIAN. ) SOLID_ANGLE_UNIT ( ) );
#16698=CARTESIAN_POINT ( 'NONE',  ( 4.000000000000000000, 2.309401076758497151, -3.433295621305379353 ) ) ;
#16709=DIRECTION ( 'NONE',  ( -0.5000000000000016653, 0.8660254037844378194, 0.000000000000000000 ) ) ;
#16713=CARTESIAN_POINT ( 'NONE',  ( 4.000000000000000000, -2.309401076758516691, -0.4999999999999995559 ) ) ;
#16722=CARTESIAN_POINT ( 'NONE',  ( 4.000000000000000000, 0.3987449864460005378, -0.01220643443059817035 ) ) ;
#16735=B_SPLINE_CURVE_WITH_KNOTS ( 'NONE', 3,
 ( #8459, #5458, #7004, #8370, #6916 ),
 .UNSPECIFIED., .F., .F.,
 ( 4, 1, 4 ),
 ( 0.000000000000000000, 0.002309401076758505790, 0.004618802153517011580 ),
 .UNSPECIFIED. ) ;
#16754=ADVANCED_FACE ( 'NONE', ( #11284 ), #7, .F. ) ;
#16770=EDGE_CURVE ( 'NONE', #11737, #18266, #2392, .T. ) ;
#16772=CARTESIAN_POINT ( 'NONE',  ( -4.211140560182196957, -2.431303136016552013, -3.745885042887436178 ) ) ;
#16817=ORIENTED_EDGE ( 'NONE', *, *, #2668, .F. ) ;
#16854=DIRECTION ( 'NONE',  ( -0.000000000000000000, -0.000000000000000000, 1.000000000000000000 ) ) ;
#16856=CARTESIAN_POINT ( 'NONE',  ( 0.000000000000000000, 0.000000000000000000, -4.974599999999998801 ) ) ;
#16891=EDGE_CURVE ( 'NONE', #12136, #12007, #17094, .T. ) ;
#16922=ORIENTED_EDGE ( 'NONE', *, *, #12697, .F. ) ;
#16929=CARTESIAN_POINT ( 'NONE',  ( -2.345747346278108214, 3.264484291692489215, -0.01223254789873409049 ) ) ;
#16961=CARTESIAN_POINT ( 'NONE',  ( -2.688821387764050996E-14, -4.618802153517012954, -0.4999999999999995559 ) ) ;
#16964=CYLINDRICAL_SURFACE ( 'NONE', #18791, 2.100000000000000089 ) ;
#16977=ORIENTED_EDGE ( 'NONE', *, *, #4961, .T. ) ;
#16987=CARTESIAN_POINT ( 'NONE',  ( 2.100000000000000089, 0.000000000000000000, -0.2800830152838844622 ) ) ;
#16988=ORIENTED_EDGE ( 'NONE', *, *, #12448, .F. ) ;
#17009=CARTESIAN_POINT ( 'NONE',  ( 0.000000000000000000, 0.000000000000000000, 0.000000000000000000 ) ) ;
#17034=CARTESIAN_POINT ( 'NONE',  ( 0.1750025118121568690, 4.719839900820621104, -3.469254087858248070 ) ) ;
#17049=( GEOMETRIC_REPRESENTATION_CONTEXT ( 3 ) GLOBAL_UNCERTAINTY_ASSIGNED_CONTEXT ( ( #1966 ) ) GLOBAL_UNIT_ASSIGNED_CONTEXT ( ( #9972, #2624, #1460 ) ) REPRESENTATION_CONTEXT ( 'NONE', 'WORKASPACE' ) );
#17060=ORIENTED_EDGE ( 'NONE', *, *, #16423, .T. ) ;
#17094=CIRCLE ( 'NONE', #8662, 5.560781378645573980 ) ;
#17100=ORIENTED_EDGE ( 'NONE', *, *, #1136, .T. ) ;
#17118=CARTESIAN_POINT ( 'NONE',  ( -4.000000000000000000, -1.942223658245633811, -0.3516579909967644246 ) ) ;
#17142=CARTESIAN_POINT ( 'NONE',  ( 0.1756481739660539498, -4.720212674038995360, -3.469390959564070620 ) ) ;
#17145=CARTESIAN_POINT ( 'NONE',  ( 5.560781378645575757, 0.000000000000000000, -4.000000000000000000 ) ) ;
#17252=CARTESIAN_POINT ( 'NONE',  ( 4.175648173966055587, -2.207990556236547608, -3.469390959564065291 ) ) ;
#17261=FACE_OUTER_BOUND ( 'NONE', #7823, .T. ) ;
#17283=EDGE_CURVE ( 'NONE', #18266, #14464, #3237, .T. ) ;
#17320=CARTESIAN_POINT ( 'NONE',  ( -4.000000000000000000, -2.309401076758512694, -5.000000000000000000 ) ) ;
#17328=ORIENTED_EDGE ( 'NONE', *, *, #178, .F. ) ;
#17331=EDGE_CURVE ( 'NONE', #5897, #1970, #14914, .T. ) ;
#17356=MECHANICAL_DESIGN_GEOMETRIC_PRESENTATION_REPRESENTATION('',(#14853),#14218);
#17413=CARTESIAN_POINT ( 'NONE',  ( 4.197393957002303999, 0.8151795401431359833, -3.503767560748935139 ) ) ;
#17427=CARTESIAN_POINT ( 'NONE',  ( 0.6666666666666689611, 4.233901974057261874, -3.300726591567082480 ) ) ;
#17499=CARTESIAN_POINT ( 'NONE',  ( -4.207491450040567571, 2.029819825146470524, -3.671670828759566074 ) ) ;
#17510=CARTESIAN_POINT ( 'NONE',  ( -2.000000000000002665, -3.464101615137770374, -3.142992957459237680 ) ) ;
#17522=ORIENTED_EDGE ( 'NONE', *, *, #13405, .F. ) ;
#17523=EDGE_CURVE ( 'NONE', #2832, #11219, #4635, .T. ) ;
#17539=CARTESIAN_POINT ( 'NONE',  ( 0.5276280594147412240, -4.314175951381924889, -3.320322319201654881 ) ) ;
#17546=CIRCLE ( 'NONE', #7553, 4.000000000000000000 ) ;
#17551=CARTESIAN_POINT ( 'NONE',  ( 1.411581201560190495E-15, 4.862606272033091592, -3.745885042887436622 ) ) ;
#17562=VERTEX_POINT ( 'NONE', #10342 ) ;
#17589=ORIENTED_EDGE ( 'NONE', *, *, #2798, .F. ) ;
#17597=B_SPLINE_CURVE_WITH_KNOTS ( 'NONE', 3,
 ( #16698, #4886, #12302, #1940, #15038, #398 ),
 .UNSPECIFIED., .F., .F.,
 ( 4, 2, 4 ),
 ( 0.000000000000000000, 0.0002095117440864783663, 0.0004190234881729567326 ),
 .UNSPECIFIED. ) ;
#17602=ADVANCED_FACE ( 'NONE', ( #14728 ), #9291, .T. ) ;
#17608=CARTESIAN_POINT ( 'NONE',  ( 0.000000000000000000, 0.000000000000000000, -4.000000000000000000 ) ) ;
#17634=VERTEX_POINT ( 'NONE', #193 ) ;
#17644=CYLINDRICAL_SURFACE ( 'NONE', #3928, 2.500000000000000444 ) ;
#17665=CARTESIAN_POINT ( 'NONE',  ( 4.000000000000000000, -1.677850389431204459, -3.535268758346977513 ) ) ;
#17692=CARTESIAN_POINT ( 'NONE',  ( 1.999999999999998224, -3.464101615137772594, -3.142992957459239012 ) ) ;
#17707=CARTESIAN_POINT ( 'NONE',  ( 1.390230914382191596, 4.043987460488659202, -3.502507215260488582 ) ) ;
#17767=CARTESIAN_POINT ( 'NONE',  ( 4.203935335434060505, 1.640780671294165272, -3.598452447879202598 ) ) ;
#17778=DIRECTION ( 'NONE',  ( -1.000000000000000000, 0.000000000000000000, 0.000000000000000000 ) ) ;
#17791=CARTESIAN_POINT ( 'NONE',  ( -4.000000000000000000, -2.472261339043343220, -3.687027428081192326 ) ) ;
#17798=PLANE ( 'NONE',  #8808 ) ;
#17887=CARTESIAN_POINT ( 'NONE',  ( -4.197477534772231955, 0.8522413273724368521, -3.505042416683225692 ) ) ;
#17908=DIRECTION ( 'NONE',  ( 1.000000000000000000, 0.000000000000000000, 0.000000000000000000 ) ) ;
#17930=DIRECTION ( 'NONE',  ( 0.8191520442889902442, 1.003171929053522651E-16, -0.5735764363510482688 ) ) ;
#17935=CARTESIAN_POINT ( 'NONE',  ( -4.000000000000000000, 2.309401076758498483, -3.433295621305379353 ) ) ;
#17983=CARTESIAN_POINT ( 'NONE',  ( -4.000000000000000000, -1.680117682357936904, -3.316611593218794951 ) ) ;
#18001=CARTESIAN_POINT ( 'NONE',  ( 3.349226789952652439, 2.685125164760731487, -0.2236248678334773199 ) ) ;
#18005=EDGE_CURVE ( 'NONE', #11737, #17562, #16735, .T. ) ;
#18024=( BOUNDED_SURFACE ( )  B_SPLINE_SURFACE ( 3, 2, ( 
 ( #4510, #5888, #13491 ),
 ( #12028, #225, #10465 ),
 ( #4613, #6179, #13202 ),
 ( #9092, #31, #17707 ),
 ( #19272, #15055, #19174 ),
 ( #16432, #10372, #4712 ) ),
 .UNSPECIFIED., .F., .F., .F. ) 
 B_SPLINE_SURFACE_WITH_KNOTS ( ( 4, 2, 4 ),
 ( 3, 3 ),
 ( 0.02032853247518126225, 0.02278863295364821212, 0.02524873343211516200 ),
 ( 0.000000000000000000, 1.000000000000000000 ),
 .UNSPECIFIED. ) 
 GEOMETRIC_REPRESENTATION_ITEM ( )  RATIONAL_B_SPLINE_SURFACE ( (
 ( 1.000000000000000000, 0.8047781615896835161, 1.000000000000000000),
 ( 1.000000000000000000, 0.8123767586291043008, 1.000000000000000000),
 ( 1.000000000000000000, 0.8190662415562011134, 1.000000000000000000),
 ( 1.000000000000000000, 0.8192361015671398849, 1.000000000000000000),
 ( 1.000000000000000000, 0.8126135807102121689, 1.000000000000000000),
 ( 1.000000000000000000, 0.8047712338318585568, 1.000000000000000000) ) ) 
 REPRESENTATION_ITEM ( '' )  SURFACE ( )  );
#18040=AXIS2_PLACEMENT_3D ( 'NONE', #16665, #1808, #15390 ) ;
#18041=LINE ( 'NONE', #4652, #3603 ) ;
#18052=CARTESIAN_POINT ( 'NONE',  ( -1.317756351988340180, 3.857995168970202116, -0.04852650426601388955 ) ) ;
#18054=AXIS2_PLACEMENT_3D ( 'NONE', #13053, #19019, #5640 ) ;
#18096=CARTESIAN_POINT ( 'NONE',  ( 4.000000000000000000, -1.942223658245635809, -0.3516579909967643691 ) ) ;
#18128=PLANE ( 'NONE',  #1111 ) ;
#18140=ORIENTED_EDGE ( 'NONE', *, *, #7977, .T. ) ;
#18175=CARTESIAN_POINT ( 'NONE',  ( -6.473970235329672780E-16, -4.862606272033106691, -3.745885042887442395 ) ) ;
#18182=DIRECTION ( 'NONE',  ( -0.8660254037844373753, 0.5000000000000021094, 0.000000000000000000 ) ) ;
#18245=CARTESIAN_POINT ( 'NONE',  ( -0.6920835326022555245, -4.454600218803899558, -3.597382984111586079 ) ) ;
#18257=CARTESIAN_POINT ( 'NONE',  ( -4.000000000000000000, 2.309401076758498483, -0.4999999999999927280 ) ) ;
#18266=VERTEX_POINT ( 'NONE', #1785 ) ;
#18271=ORIENTED_EDGE ( 'NONE', *, *, #12139, .F. ) ;
#18275=CARTESIAN_POINT ( 'NONE',  ( -2.344047193898593395, -3.265465875126480455, -1.054683074273691752E-14 ) ) ;
#18280=CARTESIAN_POINT ( 'NONE',  ( 0.000000000000000000, 0.000000000000000000, -0.2800830152838844622 ) ) ;
#18289=CARTESIAN_POINT ( 'NONE',  ( 1.655952806101427033, -3.662737355149048302, -1.182683869819604841E-14 ) ) ;
#18290=CARTESIAN_POINT ( 'NONE',  ( 4.000000000000000000, 0.9868501483902631932, -0.09357334158579604100 ) ) ;
#18291=EDGE_LOOP ( 'NONE', ( #1906, #18381, #17060, #16977, #12585 ) ) ;
#18306=ORIENTED_EDGE ( 'NONE', *, *, #14051, .T. ) ;
#18328=B_SPLINE_CURVE_WITH_KNOTS ( 'NONE', 3,
 ( #4452, #11870, #261, #11776, #17935 ),
 .UNSPECIFIED., .F., .F.,
 ( 4, 1, 4 ),
 ( 0.000000000000000000, 0.002309401076758506657, 0.004618802153517013315 ),
 .UNSPECIFIED. ) ;
#18340=VECTOR ( 'NONE', #167, 1000.000000000000000 ) ;
#18342=CARTESIAN_POINT ( 'NONE',  ( -3.861362476283256129, -2.629030857716004199, -3.671615880910374941 ) ) ;
#18352=PLANE ( 'NONE',  #6154 ) ;
#18356=ORIENTED_EDGE ( 'NONE', *, *, #11272, .F. ) ;
#18364=ORIENTED_EDGE ( 'NONE', *, *, #4224, .T. ) ;
#18371=LINE ( 'NONE', #13855, #9516 ) ;
#18381=ORIENTED_EDGE ( 'NONE', *, *, #18571, .T. ) ;
#18386=DIRECTION ( 'NONE',  ( -0.000000000000000000, 0.000000000000000000, -1.000000000000000000 ) ) ;
#18393=ORIENTED_EDGE ( 'NONE', *, *, #7168, .F. ) ;
#18404=ORIENTED_EDGE ( 'NONE', *, *, #11156, .T. ) ;
#18435=CARTESIAN_POINT ( 'NONE',  ( -6.473970235329672780E-16, -4.862606272033106691, -3.745885042887442395 ) ) ;
#18449=ORIENTED_EDGE ( 'NONE', *, *, #7478, .T. ) ;
#18451=SHAPE_DEFINITION_REPRESENTATION ( #8581, #19222 ) ;
#18454=ADVANCED_FACE ( 'NONE', ( #14372 ), #11808, .F. ) ;
#18479=CARTESIAN_POINT ( 'NONE',  ( 3.355112389629172576, -2.681727112203168950, -0.2256878752776777242 ) ) ;
#18501=ORIENTED_EDGE ( 'NONE', *, *, #11072, .F. ) ;
#18527=( BOUNDED_SURFACE ( )  B_SPLINE_SURFACE ( 3, 2, ( 
 ( #17034, #9608, #2184 ),
 ( #3738, #8239, #12921 ),
 ( #2650, #8614, #7058 ),
 ( #18892, #18794, #3832 ),
 ( #1100, #12827, #4225 ),
 ( #8712, #11649, #10181 ) ),
 .UNSPECIFIED., .F., .F., .F. ) 
 B_SPLINE_SURFACE_WITH_KNOTS ( ( 4, 2, 4 ),
 ( 3, 3 ),
 ( 0.02032853247518125531, 0.02278863295364820865, 0.02524873343211516200 ),
 ( 0.000000000000000000, 1.000000000000000000 ),
 .UNSPECIFIED. ) 
 GEOMETRIC_REPRESENTATION_ITEM ( )  RATIONAL_B_SPLINE_SURFACE ( (
 ( 1.000000000000000000, 0.8047781615896836271, 1.000000000000000000),
 ( 1.000000000000000000, 0.8123767586289967202, 1.000000000000000000),
 ( 1.000000000000000000, 0.8190662415563443322, 1.000000000000000000),
 ( 1.000000000000000000, 0.8192361015669982205, 1.000000000000000000),
 ( 1.000000000000000000, 0.8126135807103181952, 1.000000000000000000),
 ( 1.000000000000000000, 0.8047712338318587788, 1.000000000000000000) ) ) 
 REPRESENTATION_ITEM ( '' )  SURFACE ( )  );
#18549=ADVANCED_FACE ( 'NONE', ( #19169 ), #5591, .T. ) ;
#18554=EDGE_LOOP ( 'NONE', ( #4496, #9558, #335, #8195, #5120, #5145, #9511 ) ) ;
#18557=ORIENTED_EDGE ( 'NONE', *, *, #18571, .F. ) ;
#18571=EDGE_CURVE ( 'NONE', #15250, #4279, #1586, .T. ) ;
#18582=ORIENTED_EDGE ( 'NONE', *, *, #18005, .F. ) ;
#18584=CARTESIAN_POINT ( 'NONE',  ( 4.211140560182196957, -2.431303136016555122, -3.745885042887436622 ) ) ;
#18603=LINE ( 'NONE', #15571, #2631 ) ;
#18610=CIRCLE ( 'NONE', #1127, 2.100000000000000089 ) ;
#18613=CARTESIAN_POINT ( 'NONE',  ( 2.000000000000008882, 3.464101615137749945, 0.000000000000000000 ) ) ;
#18628=ORIENTED_EDGE ( 'NONE', *, *, #8869, .F. ) ;
#18657=ORIENTED_EDGE ( 'NONE', *, *, #14051, .F. ) ;
#18659=CONICAL_SURFACE ( 'NONE', #2747, 4.000000000000000000, 0.8911886515913786111 ) ;
#18679=EDGE_LOOP ( 'NONE', ( #15258, #4889, #14077, #3651, #7276 ) ) ;
#18690=B_SPLINE_CURVE_WITH_KNOTS ( 'NONE', 3,
 ( #4801, #5875, #3313, #11826, #13386, #13570 ),
 .UNSPECIFIED., .F., .F.,
 ( 4, 2, 4 ),
 ( 0.000000000000000000, 0.0002095117440864791795, 0.0004190234881729583589 ),
 .UNSPECIFIED. ) ;
#18727=DIRECTION ( 'NONE',  ( 1.000000000000000000, 0.000000000000000000, 0.000000000000000000 ) ) ;
#18734=CARTESIAN_POINT ( 'NONE',  ( 3.510273485745307731, 2.827716139362654424, -3.610536846335885564 ) ) ;
#18737=CARTESIAN_POINT ( 'NONE',  ( -4.000000000000000000, -2.309401076758512694, -5.000000000000000000 ) ) ;
#18743=DIRECTION ( 'NONE',  ( 0.000000000000000000, -1.000000000000000000, 0.000000000000000000 ) ) ;
#18762=CARTESIAN_POINT ( 'NONE',  ( 0.000000000000000000, 0.000000000000000000, -4.694516984716113228 ) ) ;
#18790=DIRECTION ( 'NONE',  ( 1.000000000000000000, 0.000000000000000000, 0.000000000000000000 ) ) ;
#18791=AXIS2_PLACEMENT_3D ( 'NONE', #664, #852, #3476 ) ;
#18794=CARTESIAN_POINT ( 'NONE',  ( -2.712762565639006418, 3.052587955997511759, -3.430618716626627318 ) ) ;
#18804=CARTESIAN_POINT ( 'NONE',  ( -4.140404888673278272, -2.228338276487456415, -3.686887068327035166 ) ) ;
#18806=CARTESIAN_POINT ( 'NONE',  ( -2.000000000000006661, 3.464101615137750834, 0.000000000000000000 ) ) ;
#18811=ADVANCED_FACE ( 'NONE', ( #16425 ), #289, .T. ) ;
#18816=EDGE_CURVE ( 'NONE', #17634, #10576, #4632, .T. ) ;
#18817=B_SPLINE_CURVE_WITH_KNOTS ( 'NONE', 3,
 ( #6114, #9129, #15092, #1708, #7663, #13618, #12163, #18613 ),
 .UNSPECIFIED., .F., .F.,
 ( 4, 2, 2, 4 ),
 ( 2.465131517075058656E-07, 0.001183067374689851080, 0.001774477805458923299, 0.002365888236227995517 ),
 .UNSPECIFIED. ) ;
#18820=CARTESIAN_POINT ( 'NONE',  ( 0.5469614295415388128, -4.303013824935362663, -3.535263753543555598 ) ) ;
#18840=ORIENTED_EDGE ( 'NONE', *, *, #5326, .F. ) ;
#18892=CARTESIAN_POINT ( 'NONE',  ( -2.725741868435985094, 3.045094352034055429, -3.220599429844047012 ) ) ;
#18940=DIRECTION ( 'NONE',  ( 0.000000000000000000, 0.000000000000000000, -1.000000000000000000 ) ) ;
#18956=AXIS2_PLACEMENT_3D ( 'NONE', #12073, #15101, #6027 ) ;
#18959=DIRECTION ( 'NONE',  ( -0.000000000000000000, -0.000000000000000000, 1.000000000000000000 ) ) ;
#18987=AXIS2_PLACEMENT_3D ( 'NONE', #1008, #6963, #5021 ) ;
#19010=CARTESIAN_POINT ( 'NONE',  ( 3.455068668934414777, -2.624017327439094327, -3.316620875263732504 ) ) ;
#19019=DIRECTION ( 'NONE',  ( -0.000000000000000000, 0.000000000000000000, -1.000000000000000000 ) ) ;
#19062=CARTESIAN_POINT ( 'NONE',  ( 4.211140560182196957, -2.431303136016555122, -3.745885042887436622 ) ) ;
#19063=ORIENTED_EDGE ( 'NONE', *, *, #3264, .F. ) ;
#19065=CARTESIAN_POINT ( 'NONE',  ( 4.000000000000000000, -2.309401076758514915, -3.433295621305383349 ) ) ;
#19098=EDGE_LOOP ( 'NONE', ( #10306, #9353, #6318 ) ) ;
#19104=CARTESIAN_POINT ( 'NONE',  ( -4.101948962586059899, -2.368261337751176754, -3.681124513963741851 ) ) ;
#19131=DIRECTION ( 'NONE',  ( 1.000000000000000000, 0.000000000000000000, 0.000000000000000000 ) ) ;
#19149=FILL_AREA_STYLE ('',( #5583 ) ) ;
#19157=CARTESIAN_POINT ( 'NONE',  ( 4.197393957002303999, -0.4069871074557456780, -3.503767560748925813 ) ) ;
#19159=CARTESIAN_POINT ( 'NONE',  ( -6.259644161404860030E-16, -4.618802153517027165, -3.433295621305388234 ) ) ;
#19169=FACE_OUTER_BOUND ( 'NONE', #1685, .T. ) ;
#19174=CARTESIAN_POINT ( 'NONE',  ( 0.6810597143197052450, 4.461075778259290914, -3.598441714920602053 ) ) ;
#19200=DIRECTION ( 'NONE',  ( -0.000000000000000000, -0.000000000000000000, 1.000000000000000000 ) ) ;
#19201=ADVANCED_FACE ( 'NONE', ( #6600 ), #6186, .T. ) ;
#19205=LINE ( 'NONE', #13330, #14923 ) ;
#19218=ORIENTED_EDGE ( 'NONE', *, *, #2668, .T. ) ;
#19222=SHAPE_REPRESENTATION ( 'hex flange nut gradea_iso_ISO - 4161 - M5 - N', ( #10540 ), #17049 ) ;
#19223=B_SPLINE_CURVE_WITH_KNOTS ( 'NONE', 3,
 ( #15206, #18245, #1915, #4862, #2013, #10906, #18342, #16772 ),
 .UNSPECIFIED., .F., .F.,
 ( 4, 2, 2, 4 ),
 ( 0.000000000000000000, 0.002450665683189818828, 0.003675998524784728459, 0.004901331366379638524 ),
 .UNSPECIFIED. ) ;
#19228=CARTESIAN_POINT ( 'NONE',  ( 4.211399257449709665, -2.459727064652517114, -3.751161691472417736 ) ) ;
#19231=CARTESIAN_POINT ( 'NONE',  ( 0.000000000000000000, 0.000000000000000000, 3.469446951953614189E-15 ) ) ;
#19256=CYLINDRICAL_SURFACE ( 'NONE', #16076, 2.100000000000000089 ) ;
#19270=DIRECTION ( 'NONE',  ( 0.000000000000000000, 0.000000000000000000, 1.000000000000000000 ) ) ;
#19272=CARTESIAN_POINT ( 'NONE',  ( 0.5449313310647804220, 4.304185902836899835, -3.316620875263383894 ) ) ;
#19279=TOROIDAL_SURFACE ( 'NONE', #18956, 5.384454397937118664, 0.5155456020628804703 ) ;
#19365=COLOUR_RGB('Black',0.12,0.14,0.17);
#19366=FILL_AREA_STYLE_COLOUR('',#19365);
#19367=FILL_AREA_STYLE('',(#19366));
#19368=SURFACE_STYLE_FILL_AREA(#19367);
#19369=SURFACE_SIDE_STYLE('',(#19368));
#19370=SURFACE_STYLE_USAGE(.BOTH.,#19369);
#19371=PRESENTATION_STYLE_ASSIGNMENT((#19370));
ENDSEC;
END-ISO-10303-21;
